ISO-10303-21;
HEADER;
/* Generated by software containing ST-Developer
 * from STEP Tools, Inc. (www.steptools.com) 
 */

FILE_DESCRIPTION(
/* description */ (''),
/* implementation_level */ '2;1');

FILE_NAME(
/* name */ 'End_Block.step',
/* time_stamp */ '2026-10-19T01:30:23+06:00',
/* author */ (''),
/* organization */ (''),
/* preprocessor_version */ 'ST-DEVELOPER v20.2',
/* originating_system */ 'Autodesk Translation Framework v15.15.0.0',
/* authorisation */ '');

FILE_SCHEMA (('AUTOMOTIVE_DESIGN { 1 0 10303 214 3 1 1 }'));
ENDSEC;

DATA;
#10=MECHANICAL_DESIGN_GEOMETRIC_PRESENTATION_REPRESENTATION('',(#90),#10639);
#51=B_SPLINE_CURVE_WITH_KNOTS('',3,(#9730,#9731,#9732,#9733,#9734,#9735,
#9736,#9737,#9738,#9739,#9740,#9741,#9742,#9743),.UNSPECIFIED.,.F.,.F.,
(4,2,2,2,2,2,4),(-0.0546723895048706,-0.0456918425711812,-0.0355825901397237,
-0.0226053755936092,-0.0114630731161328,0.,0.000317608874346033),
 .UNSPECIFIED.);
#52=B_SPLINE_CURVE_WITH_KNOTS('',3,(#9762,#9763,#9764,#9765,#9766,#9767,
#9768,#9769,#9770,#9771,#9772,#9773,#9774,#9775),.UNSPECIFIED.,.F.,.F.,
(4,2,2,2,2,2,4),(-0.0545709206888463,-0.0542557323018554,-0.0428800190516867,
-0.0318226318386046,-0.0189443163854003,-0.00891210636484469,0.),
 .UNSPECIFIED.);
#53=B_SPLINE_CURVE_WITH_KNOTS('',3,(#9781,#9782,#9783,#9784,#9785,#9786,
#9787,#9788,#9789,#9790,#9791,#9792,#9793,#9794),.UNSPECIFIED.,.F.,.F.,
(4,2,2,2,2,2,4),(-0.054570920688858,-0.0542557323018634,-0.0428800190517046,
-0.0318226318386095,-0.0189443163853947,-0.00891210636484256,0.),
 .UNSPECIFIED.);
#54=B_SPLINE_CURVE_WITH_KNOTS('',3,(#9800,#9801,#9802,#9803,#9804,#9805,
#9806,#9807,#9808,#9809,#9810,#9811,#9812,#9813),.UNSPECIFIED.,.F.,.F.,
(4,2,2,2,2,2,4),(-0.0546723899568943,-0.0456918429465685,-0.035582590428848,
-0.0226053757720057,-0.0114630731991726,0.,0.000317608880617367),
 .UNSPECIFIED.);
#55=B_SPLINE_CURVE_WITH_KNOTS('',3,(#9850,#9851,#9852,#9853,#9854,#9855,
#9856,#9857,#9858,#9859,#9860,#9861,#9862,#9863),.UNSPECIFIED.,.F.,.F.,
(4,2,2,2,2,2,4),(-0.0545709206888251,-0.0542557323018344,-0.0428800190516725,
-0.031822631838589,-0.0189443163853906,-0.00891210636484253,0.),
 .UNSPECIFIED.);
#56=B_SPLINE_CURVE_WITH_KNOTS('',3,(#9875,#9876,#9877,#9878,#9879,#9880,
#9881,#9882,#9883,#9884,#9885,#9886,#9887,#9888),.UNSPECIFIED.,.F.,.F.,
(4,2,2,2,2,2,4),(-0.0546723899569042,-0.0456918429465809,-0.0355825904288576,
-0.0226053757720114,-0.0114630731991751,0.,0.000317608880617457),
 .UNSPECIFIED.);
#57=B_SPLINE_CURVE_WITH_KNOTS('',3,(#9897,#9898,#9899,#9900,#9901,#9902,
#9903,#9904,#9905,#9906,#9907,#9908,#9909,#9910),.UNSPECIFIED.,.F.,.F.,
(4,2,2,2,2,2,4),(-0.0546723899569031,-0.0456918429465823,-0.0355825904288603,
-0.0226053757720111,-0.0114630731991739,0.,0.000317608880617373),
 .UNSPECIFIED.);
#58=B_SPLINE_CURVE_WITH_KNOTS('',3,(#9919,#9920,#9921,#9922,#9923,#9924,
#9925,#9926,#9927,#9928,#9929,#9930,#9931,#9932),.UNSPECIFIED.,.F.,.F.,
(4,2,2,2,2,2,4),(-0.0545709206996626,-0.0542557323162056,-0.0428800190513851,
-0.0318226318385961,-0.0189443163854002,-0.00891210636484565,0.),
 .UNSPECIFIED.);
#70=SHAPE_REPRESENTATION_RELATIONSHIP('SRR','None',#10680,#80);
#80=ADVANCED_BREP_SHAPE_REPRESENTATION('',(#100),#10632);
#90=STYLED_ITEM('',(#10769),#100);
#100=MANIFOLD_SOLID_BREP('End_Block',#5716);
#123=SPHERICAL_SURFACE('',#6253,0.3);
#124=SPHERICAL_SURFACE('',#6257,0.299999999999994);
#125=SPHERICAL_SURFACE('',#6261,0.300000000000011);
#126=SPHERICAL_SURFACE('',#6266,0.299999999999998);
#127=SPHERICAL_SURFACE('',#6271,0.3);
#128=SPHERICAL_SURFACE('',#6277,0.299999999999994);
#129=SPHERICAL_SURFACE('',#6282,0.3);
#130=SPHERICAL_SURFACE('',#6291,0.3);
#131=SPHERICAL_SURFACE('',#6306,0.299999999999998);
#132=SPHERICAL_SURFACE('',#6316,0.299999999999994);
#133=SPHERICAL_SURFACE('',#6321,0.299999999999994);
#134=SPHERICAL_SURFACE('',#6326,0.3);
#135=SPHERICAL_SURFACE('',#6331,0.299999999999994);
#136=SPHERICAL_SURFACE('',#6337,0.299999999999998);
#137=SPHERICAL_SURFACE('',#6341,0.300000000000002);
#138=SPHERICAL_SURFACE('',#6346,0.3);
#139=SPHERICAL_SURFACE('',#6355,0.3);
#140=SPHERICAL_SURFACE('',#6359,0.3);
#141=SPHERICAL_SURFACE('',#6363,0.3);
#142=SPHERICAL_SURFACE('',#6368,0.299999999999994);
#215=TOROIDAL_SURFACE('',#6225,2.29999999999999,0.3);
#216=TOROIDAL_SURFACE('',#6233,2.29999999999999,0.3);
#217=TOROIDAL_SURFACE('',#6238,2.29999999999999,0.3);
#218=TOROIDAL_SURFACE('',#6247,2.29999999999999,0.3);
#219=TOROIDAL_SURFACE('',#6286,0.600000000000001,0.3);
#220=TOROIDAL_SURFACE('',#6296,0.600000000000001,0.299999999999994);
#221=TOROIDAL_SURFACE('',#6301,0.600000000000001,0.299999999999976);
#222=TOROIDAL_SURFACE('',#6311,0.600000000000001,0.3);
#223=TOROIDAL_SURFACE('',#6378,4.3,0.3);
#224=TOROIDAL_SURFACE('',#6382,4.3,0.3);
#225=TOROIDAL_SURFACE('',#6385,4.3,0.3);
#226=TOROIDAL_SURFACE('',#6388,4.3,0.3);
#274=FACE_BOUND('',#973,.T.);
#275=FACE_BOUND('',#974,.T.);
#276=FACE_BOUND('',#980,.T.);
#277=FACE_BOUND('',#981,.T.);
#278=FACE_BOUND('',#1058,.T.);
#279=FACE_BOUND('',#1059,.T.);
#280=FACE_BOUND('',#1060,.T.);
#281=FACE_BOUND('',#1061,.T.);
#341=PLANE('',#6229);
#342=PLANE('',#6243);
#343=PLANE('',#6405);
#344=PLANE('',#6408);
#345=PLANE('',#6409);
#346=PLANE('',#6410);
#347=PLANE('',#6411);
#348=PLANE('',#6412);
#349=PLANE('',#6413);
#350=PLANE('',#6414);
#351=PLANE('',#6415);
#352=PLANE('',#6416);
#353=PLANE('',#6417);
#354=PLANE('',#6418);
#355=PLANE('',#6419);
#356=PLANE('',#6420);
#557=FACE_OUTER_BOUND('',#971,.T.);
#558=FACE_OUTER_BOUND('',#972,.T.);
#559=FACE_OUTER_BOUND('',#975,.T.);
#560=FACE_OUTER_BOUND('',#976,.T.);
#561=FACE_OUTER_BOUND('',#977,.T.);
#562=FACE_OUTER_BOUND('',#978,.T.);
#563=FACE_OUTER_BOUND('',#979,.T.);
#564=FACE_OUTER_BOUND('',#982,.T.);
#565=FACE_OUTER_BOUND('',#983,.T.);
#566=FACE_OUTER_BOUND('',#984,.T.);
#567=FACE_OUTER_BOUND('',#985,.T.);
#568=FACE_OUTER_BOUND('',#986,.T.);
#569=FACE_OUTER_BOUND('',#987,.T.);
#570=FACE_OUTER_BOUND('',#988,.T.);
#571=FACE_OUTER_BOUND('',#989,.T.);
#572=FACE_OUTER_BOUND('',#990,.T.);
#573=FACE_OUTER_BOUND('',#991,.T.);
#574=FACE_OUTER_BOUND('',#992,.T.);
#575=FACE_OUTER_BOUND('',#993,.T.);
#576=FACE_OUTER_BOUND('',#994,.T.);
#577=FACE_OUTER_BOUND('',#995,.T.);
#578=FACE_OUTER_BOUND('',#996,.T.);
#579=FACE_OUTER_BOUND('',#997,.T.);
#580=FACE_OUTER_BOUND('',#998,.T.);
#581=FACE_OUTER_BOUND('',#999,.T.);
#582=FACE_OUTER_BOUND('',#1000,.T.);
#583=FACE_OUTER_BOUND('',#1001,.T.);
#584=FACE_OUTER_BOUND('',#1002,.T.);
#585=FACE_OUTER_BOUND('',#1003,.T.);
#586=FACE_OUTER_BOUND('',#1004,.T.);
#587=FACE_OUTER_BOUND('',#1005,.T.);
#588=FACE_OUTER_BOUND('',#1006,.T.);
#589=FACE_OUTER_BOUND('',#1007,.T.);
#590=FACE_OUTER_BOUND('',#1008,.T.);
#591=FACE_OUTER_BOUND('',#1009,.T.);
#592=FACE_OUTER_BOUND('',#1010,.T.);
#593=FACE_OUTER_BOUND('',#1011,.T.);
#594=FACE_OUTER_BOUND('',#1012,.T.);
#595=FACE_OUTER_BOUND('',#1013,.T.);
#596=FACE_OUTER_BOUND('',#1014,.T.);
#597=FACE_OUTER_BOUND('',#1015,.T.);
#598=FACE_OUTER_BOUND('',#1016,.T.);
#599=FACE_OUTER_BOUND('',#1017,.T.);
#600=FACE_OUTER_BOUND('',#1018,.T.);
#601=FACE_OUTER_BOUND('',#1019,.T.);
#602=FACE_OUTER_BOUND('',#1020,.T.);
#603=FACE_OUTER_BOUND('',#1021,.T.);
#604=FACE_OUTER_BOUND('',#1022,.T.);
#605=FACE_OUTER_BOUND('',#1023,.T.);
#606=FACE_OUTER_BOUND('',#1024,.T.);
#607=FACE_OUTER_BOUND('',#1025,.T.);
#608=FACE_OUTER_BOUND('',#1026,.T.);
#609=FACE_OUTER_BOUND('',#1027,.T.);
#610=FACE_OUTER_BOUND('',#1028,.T.);
#611=FACE_OUTER_BOUND('',#1029,.T.);
#612=FACE_OUTER_BOUND('',#1030,.T.);
#613=FACE_OUTER_BOUND('',#1031,.T.);
#614=FACE_OUTER_BOUND('',#1032,.T.);
#615=FACE_OUTER_BOUND('',#1033,.T.);
#616=FACE_OUTER_BOUND('',#1034,.T.);
#617=FACE_OUTER_BOUND('',#1035,.T.);
#618=FACE_OUTER_BOUND('',#1036,.T.);
#619=FACE_OUTER_BOUND('',#1037,.T.);
#620=FACE_OUTER_BOUND('',#1038,.T.);
#621=FACE_OUTER_BOUND('',#1039,.T.);
#622=FACE_OUTER_BOUND('',#1040,.T.);
#623=FACE_OUTER_BOUND('',#1041,.T.);
#624=FACE_OUTER_BOUND('',#1042,.T.);
#625=FACE_OUTER_BOUND('',#1043,.T.);
#626=FACE_OUTER_BOUND('',#1044,.T.);
#627=FACE_OUTER_BOUND('',#1045,.T.);
#628=FACE_OUTER_BOUND('',#1046,.T.);
#629=FACE_OUTER_BOUND('',#1047,.T.);
#630=FACE_OUTER_BOUND('',#1048,.T.);
#631=FACE_OUTER_BOUND('',#1049,.T.);
#632=FACE_OUTER_BOUND('',#1050,.T.);
#633=FACE_OUTER_BOUND('',#1051,.T.);
#634=FACE_OUTER_BOUND('',#1052,.T.);
#635=FACE_OUTER_BOUND('',#1053,.T.);
#636=FACE_OUTER_BOUND('',#1054,.T.);
#637=FACE_OUTER_BOUND('',#1055,.T.);
#638=FACE_OUTER_BOUND('',#1056,.T.);
#639=FACE_OUTER_BOUND('',#1057,.T.);
#640=FACE_OUTER_BOUND('',#1062,.T.);
#641=FACE_OUTER_BOUND('',#1063,.T.);
#642=FACE_OUTER_BOUND('',#1064,.T.);
#643=FACE_OUTER_BOUND('',#1065,.T.);
#644=FACE_OUTER_BOUND('',#1066,.T.);
#645=FACE_OUTER_BOUND('',#1067,.T.);
#646=FACE_OUTER_BOUND('',#1068,.T.);
#647=FACE_OUTER_BOUND('',#1069,.T.);
#648=FACE_OUTER_BOUND('',#1070,.T.);
#649=FACE_OUTER_BOUND('',#1071,.T.);
#650=FACE_OUTER_BOUND('',#1072,.T.);
#971=EDGE_LOOP('',(#4270,#4271,#4272,#4273));
#972=EDGE_LOOP('',(#4274,#4275,#4276,#4277));
#973=EDGE_LOOP('',(#4278));
#974=EDGE_LOOP('',(#4279));
#975=EDGE_LOOP('',(#4280,#4281,#4282,#4283));
#976=EDGE_LOOP('',(#4284,#4285,#4286,#4287));
#977=EDGE_LOOP('',(#4288,#4289,#4290,#4291));
#978=EDGE_LOOP('',(#4292,#4293,#4294,#4295,#4296));
#979=EDGE_LOOP('',(#4297,#4298,#4299,#4300));
#980=EDGE_LOOP('',(#4301));
#981=EDGE_LOOP('',(#4302));
#982=EDGE_LOOP('',(#4303,#4304,#4305,#4306,#4307));
#983=EDGE_LOOP('',(#4308,#4309,#4310,#4311,#4312));
#984=EDGE_LOOP('',(#4313,#4314,#4315,#4316,#4317));
#985=EDGE_LOOP('',(#4318,#4319,#4320));
#986=EDGE_LOOP('',(#4321,#4322,#4323));
#987=EDGE_LOOP('',(#4324,#4325,#4326));
#988=EDGE_LOOP('',(#4327,#4328,#4329,#4330));
#989=EDGE_LOOP('',(#4331,#4332,#4333));
#990=EDGE_LOOP('',(#4334,#4335,#4336,#4337));
#991=EDGE_LOOP('',(#4338,#4339,#4340));
#992=EDGE_LOOP('',(#4341,#4342,#4343,#4344));
#993=EDGE_LOOP('',(#4345,#4346,#4347,#4348));
#994=EDGE_LOOP('',(#4349,#4350,#4351));
#995=EDGE_LOOP('',(#4352,#4353,#4354,#4355));
#996=EDGE_LOOP('',(#4356,#4357,#4358));
#997=EDGE_LOOP('',(#4359,#4360,#4361,#4362));
#998=EDGE_LOOP('',(#4363,#4364,#4365));
#999=EDGE_LOOP('',(#4366,#4367,#4368,#4369));
#1000=EDGE_LOOP('',(#4370,#4371,#4372,#4373));
#1001=EDGE_LOOP('',(#4374,#4375,#4376,#4377));
#1002=EDGE_LOOP('',(#4378,#4379,#4380));
#1003=EDGE_LOOP('',(#4381,#4382,#4383,#4384));
#1004=EDGE_LOOP('',(#4385,#4386,#4387,#4388));
#1005=EDGE_LOOP('',(#4389,#4390,#4391));
#1006=EDGE_LOOP('',(#4392,#4393,#4394,#4395));
#1007=EDGE_LOOP('',(#4396,#4397,#4398));
#1008=EDGE_LOOP('',(#4399,#4400,#4401,#4402));
#1009=EDGE_LOOP('',(#4403,#4404,#4405));
#1010=EDGE_LOOP('',(#4406,#4407,#4408,#4409));
#1011=EDGE_LOOP('',(#4410,#4411,#4412));
#1012=EDGE_LOOP('',(#4413,#4414,#4415,#4416));
#1013=EDGE_LOOP('',(#4417,#4418,#4419,#4420));
#1014=EDGE_LOOP('',(#4421,#4422,#4423));
#1015=EDGE_LOOP('',(#4424,#4425,#4426));
#1016=EDGE_LOOP('',(#4427,#4428,#4429,#4430));
#1017=EDGE_LOOP('',(#4431,#4432,#4433));
#1018=EDGE_LOOP('',(#4434,#4435,#4436,#4437));
#1019=EDGE_LOOP('',(#4438,#4439,#4440,#4441));
#1020=EDGE_LOOP('',(#4442,#4443,#4444,#4445));
#1021=EDGE_LOOP('',(#4446,#4447,#4448,#4449));
#1022=EDGE_LOOP('',(#4450,#4451,#4452,#4453));
#1023=EDGE_LOOP('',(#4454,#4455,#4456));
#1024=EDGE_LOOP('',(#4457,#4458,#4459));
#1025=EDGE_LOOP('',(#4460,#4461,#4462));
#1026=EDGE_LOOP('',(#4463,#4464,#4465,#4466));
#1027=EDGE_LOOP('',(#4467,#4468,#4469));
#1028=EDGE_LOOP('',(#4470,#4471,#4472,#4473));
#1029=EDGE_LOOP('',(#4474,#4475,#4476,#4477));
#1030=EDGE_LOOP('',(#4478,#4479,#4480,#4481));
#1031=EDGE_LOOP('',(#4482,#4483,#4484,#4485));
#1032=EDGE_LOOP('',(#4486,#4487,#4488,#4489));
#1033=EDGE_LOOP('',(#4490,#4491,#4492,#4493));
#1034=EDGE_LOOP('',(#4494,#4495,#4496,#4497));
#1035=EDGE_LOOP('',(#4498,#4499,#4500,#4501));
#1036=EDGE_LOOP('',(#4502,#4503,#4504,#4505));
#1037=EDGE_LOOP('',(#4506,#4507,#4508,#4509));
#1038=EDGE_LOOP('',(#4510,#4511,#4512,#4513));
#1039=EDGE_LOOP('',(#4514,#4515,#4516,#4517));
#1040=EDGE_LOOP('',(#4518,#4519,#4520,#4521));
#1041=EDGE_LOOP('',(#4522,#4523,#4524,#4525));
#1042=EDGE_LOOP('',(#4526,#4527,#4528,#4529));
#1043=EDGE_LOOP('',(#4530,#4531,#4532,#4533));
#1044=EDGE_LOOP('',(#4534,#4535,#4536,#4537));
#1045=EDGE_LOOP('',(#4538,#4539,#4540,#4541));
#1046=EDGE_LOOP('',(#4542,#4543,#4544,#4545));
#1047=EDGE_LOOP('',(#4546,#4547,#4548,#4549));
#1048=EDGE_LOOP('',(#4550,#4551,#4552,#4553));
#1049=EDGE_LOOP('',(#4554,#4555,#4556,#4557));
#1050=EDGE_LOOP('',(#4558,#4559,#4560,#4561));
#1051=EDGE_LOOP('',(#4562,#4563,#4564,#4565));
#1052=EDGE_LOOP('',(#4566,#4567,#4568,#4569));
#1053=EDGE_LOOP('',(#4570,#4571,#4572,#4573));
#1054=EDGE_LOOP('',(#4574,#4575,#4576,#4577));
#1055=EDGE_LOOP('',(#4578,#4579,#4580,#4581));
#1056=EDGE_LOOP('',(#4582,#4583,#4584,#4585));
#1057=EDGE_LOOP('',(#4586,#4587,#4588,#4589));
#1058=EDGE_LOOP('',(#4590));
#1059=EDGE_LOOP('',(#4591));
#1060=EDGE_LOOP('',(#4592));
#1061=EDGE_LOOP('',(#4593));
#1062=EDGE_LOOP('',(#4594,#4595,#4596,#4597));
#1063=EDGE_LOOP('',(#4598,#4599,#4600,#4601));
#1064=EDGE_LOOP('',(#4602,#4603,#4604,#4605));
#1065=EDGE_LOOP('',(#4606,#4607,#4608,#4609));
#1066=EDGE_LOOP('',(#4610,#4611,#4612,#4613));
#1067=EDGE_LOOP('',(#4614,#4615,#4616,#4617));
#1068=EDGE_LOOP('',(#4618,#4619,#4620,#4621,#4622,#4623,#4624,#4625,#4626,
#4627,#4628,#4629,#4630,#4631,#4632,#4633,#4634,#4635));
#1069=EDGE_LOOP('',(#4636,#4637,#4638,#4639));
#1070=EDGE_LOOP('',(#4640,#4641,#4642,#4643,#4644,#4645,#4646,#4647,#4648,
#4649,#4650,#4651,#4652,#4653,#4654,#4655,#4656,#4657));
#1071=EDGE_LOOP('',(#4658,#4659,#4660,#4661));
#1072=EDGE_LOOP('',(#4662,#4663,#4664,#4665));
#1351=LINE('',#9505,#1681);
#1352=LINE('',#9507,#1682);
#1353=LINE('',#9509,#1683);
#1354=LINE('',#9510,#1684);
#1355=LINE('',#9515,#1685);
#1356=LINE('',#9523,#1686);
#1357=LINE('',#9536,#1687);
#1358=LINE('',#9538,#1688);
#1359=LINE('',#9540,#1689);
#1360=LINE('',#9541,#1690);
#1361=LINE('',#9546,#1691);
#1362=LINE('',#9556,#1692);
#1363=LINE('',#9580,#1693);
#1364=LINE('',#9581,#1694);
#1365=LINE('',#9589,#1695);
#1366=LINE('',#9590,#1696);
#1367=LINE('',#9599,#1697);
#1368=LINE('',#9600,#1698);
#1369=LINE('',#9602,#1699);
#1370=LINE('',#9603,#1700);
#1371=LINE('',#9611,#1701);
#1372=LINE('',#9612,#1702);
#1373=LINE('',#9634,#1703);
#1374=LINE('',#9659,#1704);
#1375=LINE('',#9660,#1705);
#1376=LINE('',#9677,#1706);
#1377=LINE('',#9678,#1707);
#1378=LINE('',#9687,#1708);
#1379=LINE('',#9688,#1709);
#1380=LINE('',#9697,#1710);
#1381=LINE('',#9698,#1711);
#1382=LINE('',#9707,#1712);
#1383=LINE('',#9708,#1713);
#1384=LINE('',#9710,#1714);
#1385=LINE('',#9711,#1715);
#1386=LINE('',#9728,#1716);
#1387=LINE('',#9744,#1717);
#1388=LINE('',#9753,#1718);
#1389=LINE('',#9754,#1719);
#1390=LINE('',#9756,#1720);
#1391=LINE('',#9757,#1721);
#1392=LINE('',#9760,#1722);
#1393=LINE('',#9776,#1723);
#1394=LINE('',#9779,#1724);
#1395=LINE('',#9795,#1725);
#1396=LINE('',#9798,#1726);
#1397=LINE('',#9814,#1727);
#1398=LINE('',#9837,#1728);
#1399=LINE('',#9838,#1729);
#1400=LINE('',#9848,#1730);
#1401=LINE('',#9864,#1731);
#1402=LINE('',#9866,#1732);
#1403=LINE('',#9867,#1733);
#1404=LINE('',#9869,#1734);
#1405=LINE('',#9870,#1735);
#1406=LINE('',#9873,#1736);
#1407=LINE('',#9889,#1737);
#1408=LINE('',#9891,#1738);
#1409=LINE('',#9892,#1739);
#1410=LINE('',#9895,#1740);
#1411=LINE('',#9911,#1741);
#1412=LINE('',#9917,#1742);
#1413=LINE('',#9933,#1743);
#1414=LINE('',#9944,#1744);
#1415=LINE('',#9945,#1745);
#1416=LINE('',#9947,#1746);
#1417=LINE('',#9948,#1747);
#1418=LINE('',#9950,#1748);
#1419=LINE('',#9951,#1749);
#1420=LINE('',#9953,#1750);
#1421=LINE('',#9954,#1751);
#1422=LINE('',#9956,#1752);
#1423=LINE('',#9958,#1753);
#1424=LINE('',#9960,#1754);
#1425=LINE('',#9962,#1755);
#1426=LINE('',#9964,#1756);
#1427=LINE('',#9966,#1757);
#1428=LINE('',#9967,#1758);
#1429=LINE('',#9969,#1759);
#1430=LINE('',#9971,#1760);
#1431=LINE('',#9972,#1761);
#1432=LINE('',#9974,#1762);
#1433=LINE('',#9976,#1763);
#1434=LINE('',#9977,#1764);
#1435=LINE('',#9979,#1765);
#1436=LINE('',#9981,#1766);
#1437=LINE('',#9983,#1767);
#1438=LINE('',#9984,#1768);
#1681=VECTOR('',#7635,10.);
#1682=VECTOR('',#7636,10.);
#1683=VECTOR('',#7637,10.);
#1684=VECTOR('',#7638,10.);
#1685=VECTOR('',#7643,1.99999999999999);
#1686=VECTOR('',#7654,1.99999999999999);
#1687=VECTOR('',#7669,10.);
#1688=VECTOR('',#7670,10.);
#1689=VECTOR('',#7671,10.);
#1690=VECTOR('',#7672,10.);
#1691=VECTOR('',#7677,1.99999999999999);
#1692=VECTOR('',#7690,1.99999999999999);
#1693=VECTOR('',#7719,10.);
#1694=VECTOR('',#7720,10.);
#1695=VECTOR('',#7731,10.);
#1696=VECTOR('',#7732,10.);
#1697=VECTOR('',#7743,10.);
#1698=VECTOR('',#7744,10.);
#1699=VECTOR('',#7747,10.);
#1700=VECTOR('',#7748,10.);
#1701=VECTOR('',#7759,10.);
#1702=VECTOR('',#7760,10.);
#1703=VECTOR('',#7789,10.);
#1704=VECTOR('',#7820,10.);
#1705=VECTOR('',#7821,10.);
#1706=VECTOR('',#7842,10.);
#1707=VECTOR('',#7843,10.);
#1708=VECTOR('',#7854,10.);
#1709=VECTOR('',#7855,10.);
#1710=VECTOR('',#7866,10.);
#1711=VECTOR('',#7867,10.);
#1712=VECTOR('',#7878,10.);
#1713=VECTOR('',#7879,10.);
#1714=VECTOR('',#7882,10.);
#1715=VECTOR('',#7883,10.);
#1716=VECTOR('',#7902,10.);
#1717=VECTOR('',#7903,10.);
#1718=VECTOR('',#7914,10.);
#1719=VECTOR('',#7915,10.);
#1720=VECTOR('',#7918,10.);
#1721=VECTOR('',#7919,10.);
#1722=VECTOR('',#7922,10.);
#1723=VECTOR('',#7923,10.);
#1724=VECTOR('',#7926,10.);
#1725=VECTOR('',#7927,10.);
#1726=VECTOR('',#7930,10.);
#1727=VECTOR('',#7931,10.);
#1728=VECTOR('',#7958,10.);
#1729=VECTOR('',#7959,10.);
#1730=VECTOR('',#7970,10.);
#1731=VECTOR('',#7971,10.);
#1732=VECTOR('',#7974,10.);
#1733=VECTOR('',#7975,10.);
#1734=VECTOR('',#7978,10.);
#1735=VECTOR('',#7979,10.);
#1736=VECTOR('',#7982,10.);
#1737=VECTOR('',#7983,10.);
#1738=VECTOR('',#7986,10.);
#1739=VECTOR('',#7987,10.);
#1740=VECTOR('',#7990,10.);
#1741=VECTOR('',#7991,10.);
#1742=VECTOR('',#8000,10.);
#1743=VECTOR('',#8001,10.);
#1744=VECTOR('',#8022,10.);
#1745=VECTOR('',#8023,10.);
#1746=VECTOR('',#8026,10.);
#1747=VECTOR('',#8027,10.);
#1748=VECTOR('',#8030,10.);
#1749=VECTOR('',#8031,10.);
#1750=VECTOR('',#8034,10.);
#1751=VECTOR('',#8035,10.);
#1752=VECTOR('',#8038,10.);
#1753=VECTOR('',#8041,10.);
#1754=VECTOR('',#8044,10.);
#1755=VECTOR('',#8047,10.);
#1756=VECTOR('',#8050,10.);
#1757=VECTOR('',#8053,10.);
#1758=VECTOR('',#8054,10.);
#1759=VECTOR('',#8057,10.);
#1760=VECTOR('',#8060,10.);
#1761=VECTOR('',#8061,10.);
#1762=VECTOR('',#8064,10.);
#1763=VECTOR('',#8067,10.);
#1764=VECTOR('',#8068,10.);
#1765=VECTOR('',#8071,10.);
#1766=VECTOR('',#8074,10.);
#1767=VECTOR('',#8077,10.);
#1768=VECTOR('',#8078,10.);
#2060=CIRCLE('',#6226,1.99999999999999);
#2061=CIRCLE('',#6227,0.3);
#2062=CIRCLE('',#6228,2.29999999999999);
#2063=CIRCLE('',#6230,2.29999999999999);
#2064=CIRCLE('',#6232,1.99999999999999);
#2065=CIRCLE('',#6234,1.99999999999999);
#2066=CIRCLE('',#6235,0.3);
#2067=CIRCLE('',#6237,1.99999999999999);
#2068=CIRCLE('',#6239,2.29999999999999);
#2069=CIRCLE('',#6240,0.3);
#2070=CIRCLE('',#6241,1.99999999999999);
#2071=CIRCLE('',#6242,1.99999999999999);
#2072=CIRCLE('',#6244,2.29999999999999);
#2073=CIRCLE('',#6246,1.99999999999999);
#2074=CIRCLE('',#6248,0.3);
#2075=CIRCLE('',#6249,1.99999999999999);
#2076=CIRCLE('',#6250,1.99999999999999);
#2077=CIRCLE('',#6252,1.99999999999999);
#2078=CIRCLE('',#6254,0.299999999999994);
#2079=CIRCLE('',#6255,0.299999999999998);
#2080=CIRCLE('',#6256,0.3);
#2081=CIRCLE('',#6258,0.300000000000002);
#2082=CIRCLE('',#6259,0.299999999999994);
#2083=CIRCLE('',#6260,0.299999999999994);
#2084=CIRCLE('',#6262,0.3);
#2085=CIRCLE('',#6263,0.299999999999998);
#2086=CIRCLE('',#6264,0.300000000000011);
#2087=CIRCLE('',#6267,0.299999999999994);
#2088=CIRCLE('',#6268,0.299999999999998);
#2089=CIRCLE('',#6269,0.299999999999998);
#2090=CIRCLE('',#6272,0.299999999999994);
#2091=CIRCLE('',#6273,0.299999999999998);
#2092=CIRCLE('',#6274,0.3);
#2093=CIRCLE('',#6278,0.299999999999998);
#2094=CIRCLE('',#6279,0.3);
#2095=CIRCLE('',#6280,0.299999999999994);
#2096=CIRCLE('',#6283,0.299999999999994);
#2097=CIRCLE('',#6284,0.299999999999994);
#2098=CIRCLE('',#6285,0.3);
#2099=CIRCLE('',#6287,0.299999999999998);
#2100=CIRCLE('',#6288,0.3);
#2101=CIRCLE('',#6289,0.599999999999996);
#2102=CIRCLE('',#6290,0.299999999999994);
#2103=CIRCLE('',#6292,0.299999999999994);
#2104=CIRCLE('',#6293,0.299999999999994);
#2105=CIRCLE('',#6294,0.3);
#2106=CIRCLE('',#6297,0.600000000000001);
#2107=CIRCLE('',#6298,0.299999999999994);
#2108=CIRCLE('',#6299,0.3);
#2109=CIRCLE('',#6300,0.299999999999998);
#2110=CIRCLE('',#6302,0.600000000000001);
#2111=CIRCLE('',#6303,0.299999999999976);
#2112=CIRCLE('',#6304,0.3);
#2113=CIRCLE('',#6305,0.299999999999994);
#2114=CIRCLE('',#6307,0.300000000000011);
#2115=CIRCLE('',#6308,0.3);
#2116=CIRCLE('',#6309,0.299999999999998);
#2117=CIRCLE('',#6312,0.299999999999994);
#2118=CIRCLE('',#6313,0.3);
#2119=CIRCLE('',#6314,0.599999999999987);
#2120=CIRCLE('',#6315,0.299999999999994);
#2121=CIRCLE('',#6317,0.299999999999998);
#2122=CIRCLE('',#6318,0.3);
#2123=CIRCLE('',#6319,0.299999999999994);
#2124=CIRCLE('',#6322,0.300000000000002);
#2125=CIRCLE('',#6323,0.3);
#2126=CIRCLE('',#6324,0.299999999999994);
#2127=CIRCLE('',#6327,0.299999999999994);
#2128=CIRCLE('',#6328,0.299999999999998);
#2129=CIRCLE('',#6329,0.3);
#2130=CIRCLE('',#6332,0.299999999999994);
#2131=CIRCLE('',#6333,0.3);
#2132=CIRCLE('',#6334,0.299999999999994);
#2133=CIRCLE('',#6338,0.299999999999994);
#2134=CIRCLE('',#6339,0.300000000000002);
#2135=CIRCLE('',#6340,0.299999999999998);
#2136=CIRCLE('',#6342,0.299999999999998);
#2137=CIRCLE('',#6343,0.300000000000011);
#2138=CIRCLE('',#6344,0.300000000000002);
#2139=CIRCLE('',#6347,0.299999999999994);
#2140=CIRCLE('',#6348,0.299999999999998);
#2141=CIRCLE('',#6349,0.3);
#2142=CIRCLE('',#6356,0.299999999999998);
#2143=CIRCLE('',#6357,0.300000000000011);
#2144=CIRCLE('',#6358,0.3);
#2145=CIRCLE('',#6360,0.299999999999994);
#2146=CIRCLE('',#6361,0.299999999999998);
#2147=CIRCLE('',#6362,0.3);
#2148=CIRCLE('',#6364,0.299999999999994);
#2149=CIRCLE('',#6365,0.299999999999998);
#2150=CIRCLE('',#6366,0.3);
#2151=CIRCLE('',#6369,0.299999999999994);
#2152=CIRCLE('',#6370,0.3);
#2153=CIRCLE('',#6371,0.299999999999994);
#2154=CIRCLE('',#6379,4.);
#2155=CIRCLE('',#6380,4.3);
#2156=CIRCLE('',#6383,4.3);
#2157=CIRCLE('',#6384,4.);
#2158=CIRCLE('',#6386,4.3);
#2159=CIRCLE('',#6387,4.);
#2160=CIRCLE('',#6389,4.);
#2161=CIRCLE('',#6390,4.3);
#2510=VERTEX_POINT('',#9497);
#2511=VERTEX_POINT('',#9499);
#2512=VERTEX_POINT('',#9503);
#2513=VERTEX_POINT('',#9504);
#2514=VERTEX_POINT('',#9506);
#2515=VERTEX_POINT('',#9508);
#2516=VERTEX_POINT('',#9511);
#2517=VERTEX_POINT('',#9514);
#2518=VERTEX_POINT('',#9518);
#2519=VERTEX_POINT('',#9522);
#2520=VERTEX_POINT('',#9526);
#2521=VERTEX_POINT('',#9528);
#2522=VERTEX_POINT('',#9530);
#2523=VERTEX_POINT('',#9534);
#2524=VERTEX_POINT('',#9535);
#2525=VERTEX_POINT('',#9537);
#2526=VERTEX_POINT('',#9539);
#2527=VERTEX_POINT('',#9542);
#2528=VERTEX_POINT('',#9545);
#2529=VERTEX_POINT('',#9549);
#2530=VERTEX_POINT('',#9551);
#2531=VERTEX_POINT('',#9555);
#2532=VERTEX_POINT('',#9559);
#2533=VERTEX_POINT('',#9560);
#2534=VERTEX_POINT('',#9562);
#2535=VERTEX_POINT('',#9566);
#2536=VERTEX_POINT('',#9567);
#2537=VERTEX_POINT('',#9569);
#2538=VERTEX_POINT('',#9573);
#2539=VERTEX_POINT('',#9574);
#2540=VERTEX_POINT('',#9576);
#2541=VERTEX_POINT('',#9583);
#2542=VERTEX_POINT('',#9585);
#2543=VERTEX_POINT('',#9592);
#2544=VERTEX_POINT('',#9593);
#2545=VERTEX_POINT('',#9595);
#2546=VERTEX_POINT('',#9605);
#2547=VERTEX_POINT('',#9607);
#2548=VERTEX_POINT('',#9614);
#2549=VERTEX_POINT('',#9615);
#2550=VERTEX_POINT('',#9620);
#2551=VERTEX_POINT('',#9622);
#2552=VERTEX_POINT('',#9624);
#2553=VERTEX_POINT('',#9628);
#2554=VERTEX_POINT('',#9629);
#2555=VERTEX_POINT('',#9636);
#2556=VERTEX_POINT('',#9637);
#2557=VERTEX_POINT('',#9640);
#2558=VERTEX_POINT('',#9644);
#2559=VERTEX_POINT('',#9645);
#2560=VERTEX_POINT('',#9648);
#2561=VERTEX_POINT('',#9652);
#2562=VERTEX_POINT('',#9653);
#2563=VERTEX_POINT('',#9655);
#2564=VERTEX_POINT('',#9662);
#2565=VERTEX_POINT('',#9664);
#2566=VERTEX_POINT('',#9666);
#2567=VERTEX_POINT('',#9670);
#2568=VERTEX_POINT('',#9671);
#2569=VERTEX_POINT('',#9673);
#2570=VERTEX_POINT('',#9680);
#2571=VERTEX_POINT('',#9681);
#2572=VERTEX_POINT('',#9683);
#2573=VERTEX_POINT('',#9690);
#2574=VERTEX_POINT('',#9691);
#2575=VERTEX_POINT('',#9693);
#2576=VERTEX_POINT('',#9700);
#2577=VERTEX_POINT('',#9701);
#2578=VERTEX_POINT('',#9703);
#2579=VERTEX_POINT('',#9713);
#2580=VERTEX_POINT('',#9714);
#2581=VERTEX_POINT('',#9716);
#2582=VERTEX_POINT('',#9720);
#2583=VERTEX_POINT('',#9721);
#2584=VERTEX_POINT('',#9723);
#2585=VERTEX_POINT('',#9727);
#2586=VERTEX_POINT('',#9729);
#2587=VERTEX_POINT('',#9746);
#2588=VERTEX_POINT('',#9747);
#2589=VERTEX_POINT('',#9749);
#2590=VERTEX_POINT('',#9759);
#2591=VERTEX_POINT('',#9761);
#2592=VERTEX_POINT('',#9778);
#2593=VERTEX_POINT('',#9780);
#2594=VERTEX_POINT('',#9797);
#2595=VERTEX_POINT('',#9799);
#2596=VERTEX_POINT('',#9816);
#2597=VERTEX_POINT('',#9817);
#2598=VERTEX_POINT('',#9819);
#2599=VERTEX_POINT('',#9823);
#2600=VERTEX_POINT('',#9824);
#2601=VERTEX_POINT('',#9826);
#2602=VERTEX_POINT('',#9830);
#2603=VERTEX_POINT('',#9831);
#2604=VERTEX_POINT('',#9833);
#2605=VERTEX_POINT('',#9840);
#2606=VERTEX_POINT('',#9841);
#2607=VERTEX_POINT('',#9843);
#2608=VERTEX_POINT('',#9847);
#2609=VERTEX_POINT('',#9849);
#2610=VERTEX_POINT('',#9872);
#2611=VERTEX_POINT('',#9874);
#2612=VERTEX_POINT('',#9894);
#2613=VERTEX_POINT('',#9896);
#2614=VERTEX_POINT('',#9916);
#2615=VERTEX_POINT('',#9918);
#3111=EDGE_CURVE('',#2510,#2510,#2060,.T.);
#3112=EDGE_CURVE('',#2510,#2511,#2061,.T.);
#3113=EDGE_CURVE('',#2511,#2511,#2062,.T.);
#3114=EDGE_CURVE('',#2512,#2513,#1351,.T.);
#3115=EDGE_CURVE('',#2513,#2514,#1352,.T.);
#3116=EDGE_CURVE('',#2514,#2515,#1353,.T.);
#3117=EDGE_CURVE('',#2515,#2512,#1354,.T.);
#3118=EDGE_CURVE('',#2516,#2516,#2063,.T.);
#3119=EDGE_CURVE('',#2510,#2517,#1355,.T.);
#3120=EDGE_CURVE('',#2517,#2517,#2064,.T.);
#3121=EDGE_CURVE('',#2518,#2518,#2065,.T.);
#3122=EDGE_CURVE('',#2518,#2516,#2066,.T.);
#3123=EDGE_CURVE('',#2518,#2519,#1356,.T.);
#3124=EDGE_CURVE('',#2519,#2519,#2067,.T.);
#3125=EDGE_CURVE('',#2520,#2520,#2068,.T.);
#3126=EDGE_CURVE('',#2520,#2521,#2069,.T.);
#3127=EDGE_CURVE('',#2522,#2521,#2070,.T.);
#3128=EDGE_CURVE('',#2521,#2522,#2071,.T.);
#3129=EDGE_CURVE('',#2523,#2524,#1357,.T.);
#3130=EDGE_CURVE('',#2524,#2525,#1358,.T.);
#3131=EDGE_CURVE('',#2525,#2526,#1359,.T.);
#3132=EDGE_CURVE('',#2526,#2523,#1360,.T.);
#3133=EDGE_CURVE('',#2527,#2527,#2072,.T.);
#3134=EDGE_CURVE('',#2522,#2528,#1361,.T.);
#3135=EDGE_CURVE('',#2528,#2528,#2073,.T.);
#3136=EDGE_CURVE('',#2527,#2529,#2074,.T.);
#3137=EDGE_CURVE('',#2530,#2529,#2075,.T.);
#3138=EDGE_CURVE('',#2529,#2530,#2076,.T.);
#3139=EDGE_CURVE('',#2530,#2531,#1362,.T.);
#3140=EDGE_CURVE('',#2531,#2531,#2077,.T.);
#3141=EDGE_CURVE('',#2532,#2533,#2078,.F.);
#3142=EDGE_CURVE('',#2533,#2534,#2079,.F.);
#3143=EDGE_CURVE('',#2534,#2532,#2080,.F.);
#3144=EDGE_CURVE('',#2535,#2536,#2081,.F.);
#3145=EDGE_CURVE('',#2536,#2537,#2082,.F.);
#3146=EDGE_CURVE('',#2537,#2535,#2083,.F.);
#3147=EDGE_CURVE('',#2538,#2539,#2084,.F.);
#3148=EDGE_CURVE('',#2539,#2540,#2085,.F.);
#3149=EDGE_CURVE('',#2540,#2538,#2086,.F.);
#3150=EDGE_CURVE('',#2532,#2540,#1363,.T.);
#3151=EDGE_CURVE('',#2538,#2534,#1364,.T.);
#3152=EDGE_CURVE('',#2541,#2526,#2087,.F.);
#3153=EDGE_CURVE('',#2526,#2542,#2088,.F.);
#3154=EDGE_CURVE('',#2542,#2541,#2089,.F.);
#3155=EDGE_CURVE('',#2533,#2542,#1365,.T.);
#3156=EDGE_CURVE('',#2541,#2532,#1366,.T.);
#3157=EDGE_CURVE('',#2543,#2544,#2090,.F.);
#3158=EDGE_CURVE('',#2544,#2545,#2091,.F.);
#3159=EDGE_CURVE('',#2545,#2543,#2092,.F.);
#3160=EDGE_CURVE('',#2535,#2545,#1367,.T.);
#3161=EDGE_CURVE('',#2543,#2537,#1368,.T.);
#3162=EDGE_CURVE('',#2545,#2538,#1369,.T.);
#3163=EDGE_CURVE('',#2539,#2544,#1370,.T.);
#3164=EDGE_CURVE('',#2546,#2525,#2093,.F.);
#3165=EDGE_CURVE('',#2525,#2547,#2094,.F.);
#3166=EDGE_CURVE('',#2547,#2546,#2095,.F.);
#3167=EDGE_CURVE('',#2537,#2547,#1371,.T.);
#3168=EDGE_CURVE('',#2546,#2536,#1372,.T.);
#3169=EDGE_CURVE('',#2548,#2549,#2096,.F.);
#3170=EDGE_CURVE('',#2549,#2512,#2097,.F.);
#3171=EDGE_CURVE('',#2512,#2548,#2098,.F.);
#3172=EDGE_CURVE('',#2550,#2523,#2099,.F.);
#3173=EDGE_CURVE('',#2523,#2551,#2100,.T.);
#3174=EDGE_CURVE('',#2552,#2551,#2101,.T.);
#3175=EDGE_CURVE('',#2552,#2550,#2102,.T.);
#3176=EDGE_CURVE('',#2553,#2554,#2103,.F.);
#3177=EDGE_CURVE('',#2554,#2513,#2104,.F.);
#3178=EDGE_CURVE('',#2513,#2553,#2105,.F.);
#3179=EDGE_CURVE('',#2553,#2549,#1373,.T.);
#3180=EDGE_CURVE('',#2555,#2556,#2106,.T.);
#3181=EDGE_CURVE('',#2555,#2524,#2107,.T.);
#3182=EDGE_CURVE('',#2524,#2557,#2108,.F.);
#3183=EDGE_CURVE('',#2557,#2556,#2109,.T.);
#3184=EDGE_CURVE('',#2558,#2559,#2110,.T.);
#3185=EDGE_CURVE('',#2558,#2515,#2111,.T.);
#3186=EDGE_CURVE('',#2515,#2560,#2112,.F.);
#3187=EDGE_CURVE('',#2560,#2559,#2113,.T.);
#3188=EDGE_CURVE('',#2561,#2562,#2114,.F.);
#3189=EDGE_CURVE('',#2562,#2563,#2115,.F.);
#3190=EDGE_CURVE('',#2563,#2561,#2116,.F.);
#3191=EDGE_CURVE('',#2561,#2552,#1374,.T.);
#3192=EDGE_CURVE('',#2550,#2563,#1375,.T.);
#3193=EDGE_CURVE('',#2564,#2514,#2117,.F.);
#3194=EDGE_CURVE('',#2514,#2565,#2118,.T.);
#3195=EDGE_CURVE('',#2566,#2565,#2119,.T.);
#3196=EDGE_CURVE('',#2566,#2564,#2120,.T.);
#3197=EDGE_CURVE('',#2567,#2568,#2121,.F.);
#3198=EDGE_CURVE('',#2568,#2569,#2122,.F.);
#3199=EDGE_CURVE('',#2569,#2567,#2123,.F.);
#3200=EDGE_CURVE('',#2556,#2569,#1376,.T.);
#3201=EDGE_CURVE('',#2567,#2557,#1377,.T.);
#3202=EDGE_CURVE('',#2570,#2571,#2124,.F.);
#3203=EDGE_CURVE('',#2571,#2572,#2125,.F.);
#3204=EDGE_CURVE('',#2572,#2570,#2126,.F.);
#3205=EDGE_CURVE('',#2559,#2572,#1378,.T.);
#3206=EDGE_CURVE('',#2570,#2560,#1379,.T.);
#3207=EDGE_CURVE('',#2573,#2574,#2127,.F.);
#3208=EDGE_CURVE('',#2574,#2575,#2128,.F.);
#3209=EDGE_CURVE('',#2575,#2573,#2129,.F.);
#3210=EDGE_CURVE('',#2573,#2561,#1380,.T.);
#3211=EDGE_CURVE('',#2562,#2575,#1381,.T.);
#3212=EDGE_CURVE('',#2576,#2577,#2130,.F.);
#3213=EDGE_CURVE('',#2577,#2578,#2131,.F.);
#3214=EDGE_CURVE('',#2578,#2576,#2132,.F.);
#3215=EDGE_CURVE('',#2564,#2578,#1382,.T.);
#3216=EDGE_CURVE('',#2576,#2566,#1383,.T.);
#3217=EDGE_CURVE('',#2578,#2570,#1384,.T.);
#3218=EDGE_CURVE('',#2571,#2577,#1385,.T.);
#3219=EDGE_CURVE('',#2579,#2580,#2133,.F.);
#3220=EDGE_CURVE('',#2580,#2581,#2134,.F.);
#3221=EDGE_CURVE('',#2581,#2579,#2135,.F.);
#3222=EDGE_CURVE('',#2582,#2583,#2136,.F.);
#3223=EDGE_CURVE('',#2583,#2584,#2137,.F.);
#3224=EDGE_CURVE('',#2584,#2582,#2138,.F.);
#3225=EDGE_CURVE('',#2585,#2573,#1386,.T.);
#3226=EDGE_CURVE('',#2586,#2585,#51,.T.);
#3227=EDGE_CURVE('',#2574,#2586,#1387,.T.);
#3228=EDGE_CURVE('',#2587,#2588,#2139,.F.);
#3229=EDGE_CURVE('',#2588,#2589,#2140,.F.);
#3230=EDGE_CURVE('',#2589,#2587,#2141,.F.);
#3231=EDGE_CURVE('',#2587,#2576,#1388,.T.);
#3232=EDGE_CURVE('',#2577,#2589,#1389,.T.);
#3233=EDGE_CURVE('',#2582,#2588,#1390,.T.);
#3234=EDGE_CURVE('',#2589,#2584,#1391,.T.);
#3235=EDGE_CURVE('',#2590,#2581,#1392,.T.);
#3236=EDGE_CURVE('',#2591,#2590,#52,.T.);
#3237=EDGE_CURVE('',#2579,#2591,#1393,.T.);
#3238=EDGE_CURVE('',#2592,#2582,#1394,.T.);
#3239=EDGE_CURVE('',#2593,#2592,#53,.T.);
#3240=EDGE_CURVE('',#2583,#2593,#1395,.T.);
#3241=EDGE_CURVE('',#2594,#2587,#1396,.T.);
#3242=EDGE_CURVE('',#2595,#2594,#54,.T.);
#3243=EDGE_CURVE('',#2588,#2595,#1397,.T.);
#3244=EDGE_CURVE('',#2596,#2597,#2142,.F.);
#3245=EDGE_CURVE('',#2597,#2598,#2143,.F.);
#3246=EDGE_CURVE('',#2598,#2596,#2144,.F.);
#3247=EDGE_CURVE('',#2599,#2600,#2145,.F.);
#3248=EDGE_CURVE('',#2600,#2601,#2146,.F.);
#3249=EDGE_CURVE('',#2601,#2599,#2147,.F.);
#3250=EDGE_CURVE('',#2602,#2603,#2148,.F.);
#3251=EDGE_CURVE('',#2603,#2604,#2149,.F.);
#3252=EDGE_CURVE('',#2604,#2602,#2150,.F.);
#3253=EDGE_CURVE('',#2602,#2597,#1398,.T.);
#3254=EDGE_CURVE('',#2598,#2604,#1399,.T.);
#3255=EDGE_CURVE('',#2605,#2606,#2151,.F.);
#3256=EDGE_CURVE('',#2606,#2607,#2152,.F.);
#3257=EDGE_CURVE('',#2607,#2605,#2153,.F.);
#3258=EDGE_CURVE('',#2608,#2607,#1400,.T.);
#3259=EDGE_CURVE('',#2609,#2608,#55,.T.);
#3260=EDGE_CURVE('',#2605,#2609,#1401,.T.);
#3261=EDGE_CURVE('',#2607,#2603,#1402,.T.);
#3262=EDGE_CURVE('',#2604,#2606,#1403,.T.);
#3263=EDGE_CURVE('',#2599,#2605,#1404,.T.);
#3264=EDGE_CURVE('',#2606,#2601,#1405,.T.);
#3265=EDGE_CURVE('',#2610,#2602,#1406,.T.);
#3266=EDGE_CURVE('',#2611,#2610,#56,.T.);
#3267=EDGE_CURVE('',#2603,#2611,#1407,.T.);
#3268=EDGE_CURVE('',#2596,#2600,#1408,.T.);
#3269=EDGE_CURVE('',#2601,#2598,#1409,.T.);
#3270=EDGE_CURVE('',#2612,#2599,#1410,.T.);
#3271=EDGE_CURVE('',#2613,#2612,#57,.T.);
#3272=EDGE_CURVE('',#2600,#2613,#1411,.T.);
#3273=EDGE_CURVE('',#2595,#2608,#2154,.T.);
#3274=EDGE_CURVE('',#2609,#2594,#2155,.T.);
#3275=EDGE_CURVE('',#2614,#2596,#1412,.T.);
#3276=EDGE_CURVE('',#2615,#2614,#58,.T.);
#3277=EDGE_CURVE('',#2597,#2615,#1413,.T.);
#3278=EDGE_CURVE('',#2593,#2610,#2156,.T.);
#3279=EDGE_CURVE('',#2611,#2592,#2157,.T.);
#3280=EDGE_CURVE('',#2591,#2612,#2158,.T.);
#3281=EDGE_CURVE('',#2613,#2590,#2159,.T.);
#3282=EDGE_CURVE('',#2586,#2614,#2160,.T.);
#3283=EDGE_CURVE('',#2615,#2585,#2161,.T.);
#3284=EDGE_CURVE('',#2572,#2583,#1414,.T.);
#3285=EDGE_CURVE('',#2584,#2571,#1415,.T.);
#3286=EDGE_CURVE('',#2581,#2574,#1416,.T.);
#3287=EDGE_CURVE('',#2575,#2580,#1417,.T.);
#3288=EDGE_CURVE('',#2569,#2579,#1418,.T.);
#3289=EDGE_CURVE('',#2580,#2568,#1419,.T.);
#3290=EDGE_CURVE('',#2563,#2567,#1420,.T.);
#3291=EDGE_CURVE('',#2568,#2562,#1421,.T.);
#3292=EDGE_CURVE('',#2565,#2554,#1422,.T.);
#3293=EDGE_CURVE('',#2560,#2564,#1423,.T.);
#3294=EDGE_CURVE('',#2548,#2558,#1424,.T.);
#3295=EDGE_CURVE('',#2557,#2550,#1425,.T.);
#3296=EDGE_CURVE('',#2547,#2555,#1426,.T.);
#3297=EDGE_CURVE('',#2544,#2553,#1427,.T.);
#3298=EDGE_CURVE('',#2554,#2543,#1428,.T.);
#3299=EDGE_CURVE('',#2551,#2541,#1429,.T.);
#3300=EDGE_CURVE('',#2540,#2548,#1430,.T.);
#3301=EDGE_CURVE('',#2549,#2539,#1431,.T.);
#3302=EDGE_CURVE('',#2542,#2546,#1432,.T.);
#3303=EDGE_CURVE('',#2536,#2533,#1433,.T.);
#3304=EDGE_CURVE('',#2534,#2535,#1434,.T.);
#3305=EDGE_CURVE('',#2611,#2608,#1435,.T.);
#3306=EDGE_CURVE('',#2592,#2595,#1436,.T.);
#3307=EDGE_CURVE('',#2586,#2590,#1437,.T.);
#3308=EDGE_CURVE('',#2614,#2613,#1438,.T.);
#4270=ORIENTED_EDGE('',*,*,#3111,.F.);
#4271=ORIENTED_EDGE('',*,*,#3112,.T.);
#4272=ORIENTED_EDGE('',*,*,#3113,.F.);
#4273=ORIENTED_EDGE('',*,*,#3112,.F.);
#4274=ORIENTED_EDGE('',*,*,#3114,.T.);
#4275=ORIENTED_EDGE('',*,*,#3115,.T.);
#4276=ORIENTED_EDGE('',*,*,#3116,.T.);
#4277=ORIENTED_EDGE('',*,*,#3117,.T.);
#4278=ORIENTED_EDGE('',*,*,#3118,.T.);
#4279=ORIENTED_EDGE('',*,*,#3113,.T.);
#4280=ORIENTED_EDGE('',*,*,#3111,.T.);
#4281=ORIENTED_EDGE('',*,*,#3119,.T.);
#4282=ORIENTED_EDGE('',*,*,#3120,.F.);
#4283=ORIENTED_EDGE('',*,*,#3119,.F.);
#4284=ORIENTED_EDGE('',*,*,#3121,.F.);
#4285=ORIENTED_EDGE('',*,*,#3122,.T.);
#4286=ORIENTED_EDGE('',*,*,#3118,.F.);
#4287=ORIENTED_EDGE('',*,*,#3122,.F.);
#4288=ORIENTED_EDGE('',*,*,#3121,.T.);
#4289=ORIENTED_EDGE('',*,*,#3123,.T.);
#4290=ORIENTED_EDGE('',*,*,#3124,.F.);
#4291=ORIENTED_EDGE('',*,*,#3123,.F.);
#4292=ORIENTED_EDGE('',*,*,#3125,.F.);
#4293=ORIENTED_EDGE('',*,*,#3126,.T.);
#4294=ORIENTED_EDGE('',*,*,#3127,.F.);
#4295=ORIENTED_EDGE('',*,*,#3128,.F.);
#4296=ORIENTED_EDGE('',*,*,#3126,.F.);
#4297=ORIENTED_EDGE('',*,*,#3129,.T.);
#4298=ORIENTED_EDGE('',*,*,#3130,.T.);
#4299=ORIENTED_EDGE('',*,*,#3131,.T.);
#4300=ORIENTED_EDGE('',*,*,#3132,.T.);
#4301=ORIENTED_EDGE('',*,*,#3133,.T.);
#4302=ORIENTED_EDGE('',*,*,#3125,.T.);
#4303=ORIENTED_EDGE('',*,*,#3127,.T.);
#4304=ORIENTED_EDGE('',*,*,#3128,.T.);
#4305=ORIENTED_EDGE('',*,*,#3134,.T.);
#4306=ORIENTED_EDGE('',*,*,#3135,.T.);
#4307=ORIENTED_EDGE('',*,*,#3134,.F.);
#4308=ORIENTED_EDGE('',*,*,#3133,.F.);
#4309=ORIENTED_EDGE('',*,*,#3136,.T.);
#4310=ORIENTED_EDGE('',*,*,#3137,.F.);
#4311=ORIENTED_EDGE('',*,*,#3138,.F.);
#4312=ORIENTED_EDGE('',*,*,#3136,.F.);
#4313=ORIENTED_EDGE('',*,*,#3137,.T.);
#4314=ORIENTED_EDGE('',*,*,#3138,.T.);
#4315=ORIENTED_EDGE('',*,*,#3139,.T.);
#4316=ORIENTED_EDGE('',*,*,#3140,.T.);
#4317=ORIENTED_EDGE('',*,*,#3139,.F.);
#4318=ORIENTED_EDGE('',*,*,#3141,.T.);
#4319=ORIENTED_EDGE('',*,*,#3142,.T.);
#4320=ORIENTED_EDGE('',*,*,#3143,.T.);
#4321=ORIENTED_EDGE('',*,*,#3144,.T.);
#4322=ORIENTED_EDGE('',*,*,#3145,.T.);
#4323=ORIENTED_EDGE('',*,*,#3146,.T.);
#4324=ORIENTED_EDGE('',*,*,#3147,.T.);
#4325=ORIENTED_EDGE('',*,*,#3148,.T.);
#4326=ORIENTED_EDGE('',*,*,#3149,.T.);
#4327=ORIENTED_EDGE('',*,*,#3149,.F.);
#4328=ORIENTED_EDGE('',*,*,#3150,.F.);
#4329=ORIENTED_EDGE('',*,*,#3143,.F.);
#4330=ORIENTED_EDGE('',*,*,#3151,.F.);
#4331=ORIENTED_EDGE('',*,*,#3152,.T.);
#4332=ORIENTED_EDGE('',*,*,#3153,.T.);
#4333=ORIENTED_EDGE('',*,*,#3154,.T.);
#4334=ORIENTED_EDGE('',*,*,#3154,.F.);
#4335=ORIENTED_EDGE('',*,*,#3155,.F.);
#4336=ORIENTED_EDGE('',*,*,#3141,.F.);
#4337=ORIENTED_EDGE('',*,*,#3156,.F.);
#4338=ORIENTED_EDGE('',*,*,#3157,.T.);
#4339=ORIENTED_EDGE('',*,*,#3158,.T.);
#4340=ORIENTED_EDGE('',*,*,#3159,.T.);
#4341=ORIENTED_EDGE('',*,*,#3159,.F.);
#4342=ORIENTED_EDGE('',*,*,#3160,.F.);
#4343=ORIENTED_EDGE('',*,*,#3146,.F.);
#4344=ORIENTED_EDGE('',*,*,#3161,.F.);
#4345=ORIENTED_EDGE('',*,*,#3147,.F.);
#4346=ORIENTED_EDGE('',*,*,#3162,.F.);
#4347=ORIENTED_EDGE('',*,*,#3158,.F.);
#4348=ORIENTED_EDGE('',*,*,#3163,.F.);
#4349=ORIENTED_EDGE('',*,*,#3164,.T.);
#4350=ORIENTED_EDGE('',*,*,#3165,.T.);
#4351=ORIENTED_EDGE('',*,*,#3166,.T.);
#4352=ORIENTED_EDGE('',*,*,#3166,.F.);
#4353=ORIENTED_EDGE('',*,*,#3167,.F.);
#4354=ORIENTED_EDGE('',*,*,#3145,.F.);
#4355=ORIENTED_EDGE('',*,*,#3168,.F.);
#4356=ORIENTED_EDGE('',*,*,#3169,.T.);
#4357=ORIENTED_EDGE('',*,*,#3170,.T.);
#4358=ORIENTED_EDGE('',*,*,#3171,.T.);
#4359=ORIENTED_EDGE('',*,*,#3172,.T.);
#4360=ORIENTED_EDGE('',*,*,#3173,.T.);
#4361=ORIENTED_EDGE('',*,*,#3174,.F.);
#4362=ORIENTED_EDGE('',*,*,#3175,.T.);
#4363=ORIENTED_EDGE('',*,*,#3176,.T.);
#4364=ORIENTED_EDGE('',*,*,#3177,.T.);
#4365=ORIENTED_EDGE('',*,*,#3178,.T.);
#4366=ORIENTED_EDGE('',*,*,#3178,.F.);
#4367=ORIENTED_EDGE('',*,*,#3114,.F.);
#4368=ORIENTED_EDGE('',*,*,#3170,.F.);
#4369=ORIENTED_EDGE('',*,*,#3179,.F.);
#4370=ORIENTED_EDGE('',*,*,#3180,.F.);
#4371=ORIENTED_EDGE('',*,*,#3181,.T.);
#4372=ORIENTED_EDGE('',*,*,#3182,.T.);
#4373=ORIENTED_EDGE('',*,*,#3183,.T.);
#4374=ORIENTED_EDGE('',*,*,#3184,.F.);
#4375=ORIENTED_EDGE('',*,*,#3185,.T.);
#4376=ORIENTED_EDGE('',*,*,#3186,.T.);
#4377=ORIENTED_EDGE('',*,*,#3187,.T.);
#4378=ORIENTED_EDGE('',*,*,#3188,.T.);
#4379=ORIENTED_EDGE('',*,*,#3189,.T.);
#4380=ORIENTED_EDGE('',*,*,#3190,.T.);
#4381=ORIENTED_EDGE('',*,*,#3175,.F.);
#4382=ORIENTED_EDGE('',*,*,#3191,.F.);
#4383=ORIENTED_EDGE('',*,*,#3190,.F.);
#4384=ORIENTED_EDGE('',*,*,#3192,.F.);
#4385=ORIENTED_EDGE('',*,*,#3193,.T.);
#4386=ORIENTED_EDGE('',*,*,#3194,.T.);
#4387=ORIENTED_EDGE('',*,*,#3195,.F.);
#4388=ORIENTED_EDGE('',*,*,#3196,.T.);
#4389=ORIENTED_EDGE('',*,*,#3197,.T.);
#4390=ORIENTED_EDGE('',*,*,#3198,.T.);
#4391=ORIENTED_EDGE('',*,*,#3199,.T.);
#4392=ORIENTED_EDGE('',*,*,#3199,.F.);
#4393=ORIENTED_EDGE('',*,*,#3200,.F.);
#4394=ORIENTED_EDGE('',*,*,#3183,.F.);
#4395=ORIENTED_EDGE('',*,*,#3201,.F.);
#4396=ORIENTED_EDGE('',*,*,#3202,.T.);
#4397=ORIENTED_EDGE('',*,*,#3203,.T.);
#4398=ORIENTED_EDGE('',*,*,#3204,.T.);
#4399=ORIENTED_EDGE('',*,*,#3204,.F.);
#4400=ORIENTED_EDGE('',*,*,#3205,.F.);
#4401=ORIENTED_EDGE('',*,*,#3187,.F.);
#4402=ORIENTED_EDGE('',*,*,#3206,.F.);
#4403=ORIENTED_EDGE('',*,*,#3207,.T.);
#4404=ORIENTED_EDGE('',*,*,#3208,.T.);
#4405=ORIENTED_EDGE('',*,*,#3209,.T.);
#4406=ORIENTED_EDGE('',*,*,#3188,.F.);
#4407=ORIENTED_EDGE('',*,*,#3210,.F.);
#4408=ORIENTED_EDGE('',*,*,#3209,.F.);
#4409=ORIENTED_EDGE('',*,*,#3211,.F.);
#4410=ORIENTED_EDGE('',*,*,#3212,.T.);
#4411=ORIENTED_EDGE('',*,*,#3213,.T.);
#4412=ORIENTED_EDGE('',*,*,#3214,.T.);
#4413=ORIENTED_EDGE('',*,*,#3214,.F.);
#4414=ORIENTED_EDGE('',*,*,#3215,.F.);
#4415=ORIENTED_EDGE('',*,*,#3196,.F.);
#4416=ORIENTED_EDGE('',*,*,#3216,.F.);
#4417=ORIENTED_EDGE('',*,*,#3202,.F.);
#4418=ORIENTED_EDGE('',*,*,#3217,.F.);
#4419=ORIENTED_EDGE('',*,*,#3213,.F.);
#4420=ORIENTED_EDGE('',*,*,#3218,.F.);
#4421=ORIENTED_EDGE('',*,*,#3219,.T.);
#4422=ORIENTED_EDGE('',*,*,#3220,.T.);
#4423=ORIENTED_EDGE('',*,*,#3221,.T.);
#4424=ORIENTED_EDGE('',*,*,#3222,.T.);
#4425=ORIENTED_EDGE('',*,*,#3223,.T.);
#4426=ORIENTED_EDGE('',*,*,#3224,.T.);
#4427=ORIENTED_EDGE('',*,*,#3225,.F.);
#4428=ORIENTED_EDGE('',*,*,#3226,.F.);
#4429=ORIENTED_EDGE('',*,*,#3227,.F.);
#4430=ORIENTED_EDGE('',*,*,#3207,.F.);
#4431=ORIENTED_EDGE('',*,*,#3228,.T.);
#4432=ORIENTED_EDGE('',*,*,#3229,.T.);
#4433=ORIENTED_EDGE('',*,*,#3230,.T.);
#4434=ORIENTED_EDGE('',*,*,#3212,.F.);
#4435=ORIENTED_EDGE('',*,*,#3231,.F.);
#4436=ORIENTED_EDGE('',*,*,#3230,.F.);
#4437=ORIENTED_EDGE('',*,*,#3232,.F.);
#4438=ORIENTED_EDGE('',*,*,#3229,.F.);
#4439=ORIENTED_EDGE('',*,*,#3233,.F.);
#4440=ORIENTED_EDGE('',*,*,#3224,.F.);
#4441=ORIENTED_EDGE('',*,*,#3234,.F.);
#4442=ORIENTED_EDGE('',*,*,#3235,.F.);
#4443=ORIENTED_EDGE('',*,*,#3236,.F.);
#4444=ORIENTED_EDGE('',*,*,#3237,.F.);
#4445=ORIENTED_EDGE('',*,*,#3221,.F.);
#4446=ORIENTED_EDGE('',*,*,#3238,.F.);
#4447=ORIENTED_EDGE('',*,*,#3239,.F.);
#4448=ORIENTED_EDGE('',*,*,#3240,.F.);
#4449=ORIENTED_EDGE('',*,*,#3222,.F.);
#4450=ORIENTED_EDGE('',*,*,#3241,.F.);
#4451=ORIENTED_EDGE('',*,*,#3242,.F.);
#4452=ORIENTED_EDGE('',*,*,#3243,.F.);
#4453=ORIENTED_EDGE('',*,*,#3228,.F.);
#4454=ORIENTED_EDGE('',*,*,#3244,.T.);
#4455=ORIENTED_EDGE('',*,*,#3245,.T.);
#4456=ORIENTED_EDGE('',*,*,#3246,.T.);
#4457=ORIENTED_EDGE('',*,*,#3247,.T.);
#4458=ORIENTED_EDGE('',*,*,#3248,.T.);
#4459=ORIENTED_EDGE('',*,*,#3249,.T.);
#4460=ORIENTED_EDGE('',*,*,#3250,.T.);
#4461=ORIENTED_EDGE('',*,*,#3251,.T.);
#4462=ORIENTED_EDGE('',*,*,#3252,.T.);
#4463=ORIENTED_EDGE('',*,*,#3245,.F.);
#4464=ORIENTED_EDGE('',*,*,#3253,.F.);
#4465=ORIENTED_EDGE('',*,*,#3252,.F.);
#4466=ORIENTED_EDGE('',*,*,#3254,.F.);
#4467=ORIENTED_EDGE('',*,*,#3255,.T.);
#4468=ORIENTED_EDGE('',*,*,#3256,.T.);
#4469=ORIENTED_EDGE('',*,*,#3257,.T.);
#4470=ORIENTED_EDGE('',*,*,#3258,.F.);
#4471=ORIENTED_EDGE('',*,*,#3259,.F.);
#4472=ORIENTED_EDGE('',*,*,#3260,.F.);
#4473=ORIENTED_EDGE('',*,*,#3257,.F.);
#4474=ORIENTED_EDGE('',*,*,#3251,.F.);
#4475=ORIENTED_EDGE('',*,*,#3261,.F.);
#4476=ORIENTED_EDGE('',*,*,#3256,.F.);
#4477=ORIENTED_EDGE('',*,*,#3262,.F.);
#4478=ORIENTED_EDGE('',*,*,#3255,.F.);
#4479=ORIENTED_EDGE('',*,*,#3263,.F.);
#4480=ORIENTED_EDGE('',*,*,#3249,.F.);
#4481=ORIENTED_EDGE('',*,*,#3264,.F.);
#4482=ORIENTED_EDGE('',*,*,#3265,.F.);
#4483=ORIENTED_EDGE('',*,*,#3266,.F.);
#4484=ORIENTED_EDGE('',*,*,#3267,.F.);
#4485=ORIENTED_EDGE('',*,*,#3250,.F.);
#4486=ORIENTED_EDGE('',*,*,#3248,.F.);
#4487=ORIENTED_EDGE('',*,*,#3268,.F.);
#4488=ORIENTED_EDGE('',*,*,#3246,.F.);
#4489=ORIENTED_EDGE('',*,*,#3269,.F.);
#4490=ORIENTED_EDGE('',*,*,#3270,.F.);
#4491=ORIENTED_EDGE('',*,*,#3271,.F.);
#4492=ORIENTED_EDGE('',*,*,#3272,.F.);
#4493=ORIENTED_EDGE('',*,*,#3247,.F.);
#4494=ORIENTED_EDGE('',*,*,#3273,.F.);
#4495=ORIENTED_EDGE('',*,*,#3242,.T.);
#4496=ORIENTED_EDGE('',*,*,#3274,.F.);
#4497=ORIENTED_EDGE('',*,*,#3259,.T.);
#4498=ORIENTED_EDGE('',*,*,#3275,.F.);
#4499=ORIENTED_EDGE('',*,*,#3276,.F.);
#4500=ORIENTED_EDGE('',*,*,#3277,.F.);
#4501=ORIENTED_EDGE('',*,*,#3244,.F.);
#4502=ORIENTED_EDGE('',*,*,#3278,.F.);
#4503=ORIENTED_EDGE('',*,*,#3239,.T.);
#4504=ORIENTED_EDGE('',*,*,#3279,.F.);
#4505=ORIENTED_EDGE('',*,*,#3266,.T.);
#4506=ORIENTED_EDGE('',*,*,#3280,.F.);
#4507=ORIENTED_EDGE('',*,*,#3236,.T.);
#4508=ORIENTED_EDGE('',*,*,#3281,.F.);
#4509=ORIENTED_EDGE('',*,*,#3271,.T.);
#4510=ORIENTED_EDGE('',*,*,#3282,.F.);
#4511=ORIENTED_EDGE('',*,*,#3226,.T.);
#4512=ORIENTED_EDGE('',*,*,#3283,.F.);
#4513=ORIENTED_EDGE('',*,*,#3276,.T.);
#4514=ORIENTED_EDGE('',*,*,#3223,.F.);
#4515=ORIENTED_EDGE('',*,*,#3284,.F.);
#4516=ORIENTED_EDGE('',*,*,#3203,.F.);
#4517=ORIENTED_EDGE('',*,*,#3285,.F.);
#4518=ORIENTED_EDGE('',*,*,#3208,.F.);
#4519=ORIENTED_EDGE('',*,*,#3286,.F.);
#4520=ORIENTED_EDGE('',*,*,#3220,.F.);
#4521=ORIENTED_EDGE('',*,*,#3287,.F.);
#4522=ORIENTED_EDGE('',*,*,#3219,.F.);
#4523=ORIENTED_EDGE('',*,*,#3288,.F.);
#4524=ORIENTED_EDGE('',*,*,#3198,.F.);
#4525=ORIENTED_EDGE('',*,*,#3289,.F.);
#4526=ORIENTED_EDGE('',*,*,#3197,.F.);
#4527=ORIENTED_EDGE('',*,*,#3290,.F.);
#4528=ORIENTED_EDGE('',*,*,#3189,.F.);
#4529=ORIENTED_EDGE('',*,*,#3291,.F.);
#4530=ORIENTED_EDGE('',*,*,#3194,.F.);
#4531=ORIENTED_EDGE('',*,*,#3115,.F.);
#4532=ORIENTED_EDGE('',*,*,#3177,.F.);
#4533=ORIENTED_EDGE('',*,*,#3292,.F.);
#4534=ORIENTED_EDGE('',*,*,#3186,.F.);
#4535=ORIENTED_EDGE('',*,*,#3116,.F.);
#4536=ORIENTED_EDGE('',*,*,#3193,.F.);
#4537=ORIENTED_EDGE('',*,*,#3293,.F.);
#4538=ORIENTED_EDGE('',*,*,#3171,.F.);
#4539=ORIENTED_EDGE('',*,*,#3117,.F.);
#4540=ORIENTED_EDGE('',*,*,#3185,.F.);
#4541=ORIENTED_EDGE('',*,*,#3294,.F.);
#4542=ORIENTED_EDGE('',*,*,#3182,.F.);
#4543=ORIENTED_EDGE('',*,*,#3129,.F.);
#4544=ORIENTED_EDGE('',*,*,#3172,.F.);
#4545=ORIENTED_EDGE('',*,*,#3295,.F.);
#4546=ORIENTED_EDGE('',*,*,#3181,.F.);
#4547=ORIENTED_EDGE('',*,*,#3296,.F.);
#4548=ORIENTED_EDGE('',*,*,#3165,.F.);
#4549=ORIENTED_EDGE('',*,*,#3130,.F.);
#4550=ORIENTED_EDGE('',*,*,#3176,.F.);
#4551=ORIENTED_EDGE('',*,*,#3297,.F.);
#4552=ORIENTED_EDGE('',*,*,#3157,.F.);
#4553=ORIENTED_EDGE('',*,*,#3298,.F.);
#4554=ORIENTED_EDGE('',*,*,#3152,.F.);
#4555=ORIENTED_EDGE('',*,*,#3299,.F.);
#4556=ORIENTED_EDGE('',*,*,#3173,.F.);
#4557=ORIENTED_EDGE('',*,*,#3132,.F.);
#4558=ORIENTED_EDGE('',*,*,#3169,.F.);
#4559=ORIENTED_EDGE('',*,*,#3300,.F.);
#4560=ORIENTED_EDGE('',*,*,#3148,.F.);
#4561=ORIENTED_EDGE('',*,*,#3301,.F.);
#4562=ORIENTED_EDGE('',*,*,#3164,.F.);
#4563=ORIENTED_EDGE('',*,*,#3302,.F.);
#4564=ORIENTED_EDGE('',*,*,#3153,.F.);
#4565=ORIENTED_EDGE('',*,*,#3131,.F.);
#4566=ORIENTED_EDGE('',*,*,#3142,.F.);
#4567=ORIENTED_EDGE('',*,*,#3303,.F.);
#4568=ORIENTED_EDGE('',*,*,#3144,.F.);
#4569=ORIENTED_EDGE('',*,*,#3304,.F.);
#4570=ORIENTED_EDGE('',*,*,#3267,.T.);
#4571=ORIENTED_EDGE('',*,*,#3305,.T.);
#4572=ORIENTED_EDGE('',*,*,#3258,.T.);
#4573=ORIENTED_EDGE('',*,*,#3261,.T.);
#4574=ORIENTED_EDGE('',*,*,#3279,.T.);
#4575=ORIENTED_EDGE('',*,*,#3306,.T.);
#4576=ORIENTED_EDGE('',*,*,#3273,.T.);
#4577=ORIENTED_EDGE('',*,*,#3305,.F.);
#4578=ORIENTED_EDGE('',*,*,#3281,.T.);
#4579=ORIENTED_EDGE('',*,*,#3307,.F.);
#4580=ORIENTED_EDGE('',*,*,#3282,.T.);
#4581=ORIENTED_EDGE('',*,*,#3308,.T.);
#4582=ORIENTED_EDGE('',*,*,#3272,.T.);
#4583=ORIENTED_EDGE('',*,*,#3308,.F.);
#4584=ORIENTED_EDGE('',*,*,#3275,.T.);
#4585=ORIENTED_EDGE('',*,*,#3268,.T.);
#4586=ORIENTED_EDGE('',*,*,#3160,.T.);
#4587=ORIENTED_EDGE('',*,*,#3162,.T.);
#4588=ORIENTED_EDGE('',*,*,#3151,.T.);
#4589=ORIENTED_EDGE('',*,*,#3304,.T.);
#4590=ORIENTED_EDGE('',*,*,#3140,.F.);
#4591=ORIENTED_EDGE('',*,*,#3135,.F.);
#4592=ORIENTED_EDGE('',*,*,#3124,.T.);
#4593=ORIENTED_EDGE('',*,*,#3120,.T.);
#4594=ORIENTED_EDGE('',*,*,#3168,.T.);
#4595=ORIENTED_EDGE('',*,*,#3303,.T.);
#4596=ORIENTED_EDGE('',*,*,#3155,.T.);
#4597=ORIENTED_EDGE('',*,*,#3302,.T.);
#4598=ORIENTED_EDGE('',*,*,#3179,.T.);
#4599=ORIENTED_EDGE('',*,*,#3301,.T.);
#4600=ORIENTED_EDGE('',*,*,#3163,.T.);
#4601=ORIENTED_EDGE('',*,*,#3297,.T.);
#4602=ORIENTED_EDGE('',*,*,#3201,.T.);
#4603=ORIENTED_EDGE('',*,*,#3295,.T.);
#4604=ORIENTED_EDGE('',*,*,#3192,.T.);
#4605=ORIENTED_EDGE('',*,*,#3290,.T.);
#4606=ORIENTED_EDGE('',*,*,#3211,.T.);
#4607=ORIENTED_EDGE('',*,*,#3287,.T.);
#4608=ORIENTED_EDGE('',*,*,#3289,.T.);
#4609=ORIENTED_EDGE('',*,*,#3291,.T.);
#4610=ORIENTED_EDGE('',*,*,#3215,.T.);
#4611=ORIENTED_EDGE('',*,*,#3217,.T.);
#4612=ORIENTED_EDGE('',*,*,#3206,.T.);
#4613=ORIENTED_EDGE('',*,*,#3293,.T.);
#4614=ORIENTED_EDGE('',*,*,#3218,.T.);
#4615=ORIENTED_EDGE('',*,*,#3232,.T.);
#4616=ORIENTED_EDGE('',*,*,#3234,.T.);
#4617=ORIENTED_EDGE('',*,*,#3285,.T.);
#4618=ORIENTED_EDGE('',*,*,#3253,.T.);
#4619=ORIENTED_EDGE('',*,*,#3277,.T.);
#4620=ORIENTED_EDGE('',*,*,#3283,.T.);
#4621=ORIENTED_EDGE('',*,*,#3225,.T.);
#4622=ORIENTED_EDGE('',*,*,#3210,.T.);
#4623=ORIENTED_EDGE('',*,*,#3191,.T.);
#4624=ORIENTED_EDGE('',*,*,#3174,.T.);
#4625=ORIENTED_EDGE('',*,*,#3299,.T.);
#4626=ORIENTED_EDGE('',*,*,#3156,.T.);
#4627=ORIENTED_EDGE('',*,*,#3150,.T.);
#4628=ORIENTED_EDGE('',*,*,#3300,.T.);
#4629=ORIENTED_EDGE('',*,*,#3294,.T.);
#4630=ORIENTED_EDGE('',*,*,#3184,.T.);
#4631=ORIENTED_EDGE('',*,*,#3205,.T.);
#4632=ORIENTED_EDGE('',*,*,#3284,.T.);
#4633=ORIENTED_EDGE('',*,*,#3240,.T.);
#4634=ORIENTED_EDGE('',*,*,#3278,.T.);
#4635=ORIENTED_EDGE('',*,*,#3265,.T.);
#4636=ORIENTED_EDGE('',*,*,#3254,.T.);
#4637=ORIENTED_EDGE('',*,*,#3262,.T.);
#4638=ORIENTED_EDGE('',*,*,#3264,.T.);
#4639=ORIENTED_EDGE('',*,*,#3269,.T.);
#4640=ORIENTED_EDGE('',*,*,#3260,.T.);
#4641=ORIENTED_EDGE('',*,*,#3274,.T.);
#4642=ORIENTED_EDGE('',*,*,#3241,.T.);
#4643=ORIENTED_EDGE('',*,*,#3231,.T.);
#4644=ORIENTED_EDGE('',*,*,#3216,.T.);
#4645=ORIENTED_EDGE('',*,*,#3195,.T.);
#4646=ORIENTED_EDGE('',*,*,#3292,.T.);
#4647=ORIENTED_EDGE('',*,*,#3298,.T.);
#4648=ORIENTED_EDGE('',*,*,#3161,.T.);
#4649=ORIENTED_EDGE('',*,*,#3167,.T.);
#4650=ORIENTED_EDGE('',*,*,#3296,.T.);
#4651=ORIENTED_EDGE('',*,*,#3180,.T.);
#4652=ORIENTED_EDGE('',*,*,#3200,.T.);
#4653=ORIENTED_EDGE('',*,*,#3288,.T.);
#4654=ORIENTED_EDGE('',*,*,#3237,.T.);
#4655=ORIENTED_EDGE('',*,*,#3280,.T.);
#4656=ORIENTED_EDGE('',*,*,#3270,.T.);
#4657=ORIENTED_EDGE('',*,*,#3263,.T.);
#4658=ORIENTED_EDGE('',*,*,#3238,.T.);
#4659=ORIENTED_EDGE('',*,*,#3233,.T.);
#4660=ORIENTED_EDGE('',*,*,#3243,.T.);
#4661=ORIENTED_EDGE('',*,*,#3306,.F.);
#4662=ORIENTED_EDGE('',*,*,#3235,.T.);
#4663=ORIENTED_EDGE('',*,*,#3286,.T.);
#4664=ORIENTED_EDGE('',*,*,#3227,.T.);
#4665=ORIENTED_EDGE('',*,*,#3307,.T.);
#5227=CYLINDRICAL_SURFACE('',#6231,1.99999999999999);
#5228=CYLINDRICAL_SURFACE('',#6236,1.99999999999999);
#5229=CYLINDRICAL_SURFACE('',#6245,1.99999999999999);
#5230=CYLINDRICAL_SURFACE('',#6251,1.99999999999999);
#5231=CYLINDRICAL_SURFACE('',#6265,0.3);
#5232=CYLINDRICAL_SURFACE('',#6270,0.3);
#5233=CYLINDRICAL_SURFACE('',#6275,0.3);
#5234=CYLINDRICAL_SURFACE('',#6276,0.3);
#5235=CYLINDRICAL_SURFACE('',#6281,0.3);
#5236=CYLINDRICAL_SURFACE('',#6295,0.3);
#5237=CYLINDRICAL_SURFACE('',#6310,0.3);
#5238=CYLINDRICAL_SURFACE('',#6320,0.3);
#5239=CYLINDRICAL_SURFACE('',#6325,0.3);
#5240=CYLINDRICAL_SURFACE('',#6330,0.3);
#5241=CYLINDRICAL_SURFACE('',#6335,0.3);
#5242=CYLINDRICAL_SURFACE('',#6336,0.3);
#5243=CYLINDRICAL_SURFACE('',#6345,0.3);
#5244=CYLINDRICAL_SURFACE('',#6350,0.3);
#5245=CYLINDRICAL_SURFACE('',#6351,0.3);
#5246=CYLINDRICAL_SURFACE('',#6352,0.3);
#5247=CYLINDRICAL_SURFACE('',#6353,0.3);
#5248=CYLINDRICAL_SURFACE('',#6354,0.3);
#5249=CYLINDRICAL_SURFACE('',#6367,0.3);
#5250=CYLINDRICAL_SURFACE('',#6372,0.3);
#5251=CYLINDRICAL_SURFACE('',#6373,0.3);
#5252=CYLINDRICAL_SURFACE('',#6374,0.3);
#5253=CYLINDRICAL_SURFACE('',#6375,0.3);
#5254=CYLINDRICAL_SURFACE('',#6376,0.3);
#5255=CYLINDRICAL_SURFACE('',#6377,0.3);
#5256=CYLINDRICAL_SURFACE('',#6381,0.3);
#5257=CYLINDRICAL_SURFACE('',#6391,0.3);
#5258=CYLINDRICAL_SURFACE('',#6392,0.3);
#5259=CYLINDRICAL_SURFACE('',#6393,0.3);
#5260=CYLINDRICAL_SURFACE('',#6394,0.3);
#5261=CYLINDRICAL_SURFACE('',#6395,0.3);
#5262=CYLINDRICAL_SURFACE('',#6396,0.3);
#5263=CYLINDRICAL_SURFACE('',#6397,0.3);
#5264=CYLINDRICAL_SURFACE('',#6398,0.3);
#5265=CYLINDRICAL_SURFACE('',#6399,0.3);
#5266=CYLINDRICAL_SURFACE('',#6400,0.3);
#5267=CYLINDRICAL_SURFACE('',#6401,0.3);
#5268=CYLINDRICAL_SURFACE('',#6402,0.3);
#5269=CYLINDRICAL_SURFACE('',#6403,0.3);
#5270=CYLINDRICAL_SURFACE('',#6404,0.3);
#5271=CYLINDRICAL_SURFACE('',#6406,4.);
#5272=CYLINDRICAL_SURFACE('',#6407,4.);
#5500=ADVANCED_FACE('',(#557),#215,.T.);
#5501=ADVANCED_FACE('',(#558,#274,#275),#341,.F.);
#5502=ADVANCED_FACE('',(#559),#5227,.F.);
#5503=ADVANCED_FACE('',(#560),#216,.T.);
#5504=ADVANCED_FACE('',(#561),#5228,.F.);
#5505=ADVANCED_FACE('',(#562),#217,.T.);
#5506=ADVANCED_FACE('',(#563,#276,#277),#342,.T.);
#5507=ADVANCED_FACE('',(#564),#5229,.F.);
#5508=ADVANCED_FACE('',(#565),#218,.T.);
#5509=ADVANCED_FACE('',(#566),#5230,.F.);
#5510=ADVANCED_FACE('',(#567),#123,.T.);
#5511=ADVANCED_FACE('',(#568),#124,.T.);
#5512=ADVANCED_FACE('',(#569),#125,.T.);
#5513=ADVANCED_FACE('',(#570),#5231,.T.);
#5514=ADVANCED_FACE('',(#571),#126,.T.);
#5515=ADVANCED_FACE('',(#572),#5232,.T.);
#5516=ADVANCED_FACE('',(#573),#127,.T.);
#5517=ADVANCED_FACE('',(#574),#5233,.T.);
#5518=ADVANCED_FACE('',(#575),#5234,.T.);
#5519=ADVANCED_FACE('',(#576),#128,.T.);
#5520=ADVANCED_FACE('',(#577),#5235,.T.);
#5521=ADVANCED_FACE('',(#578),#129,.T.);
#5522=ADVANCED_FACE('',(#579),#219,.T.);
#5523=ADVANCED_FACE('',(#580),#130,.T.);
#5524=ADVANCED_FACE('',(#581),#5236,.T.);
#5525=ADVANCED_FACE('',(#582),#220,.T.);
#5526=ADVANCED_FACE('',(#583),#221,.T.);
#5527=ADVANCED_FACE('',(#584),#131,.T.);
#5528=ADVANCED_FACE('',(#585),#5237,.T.);
#5529=ADVANCED_FACE('',(#586),#222,.T.);
#5530=ADVANCED_FACE('',(#587),#132,.T.);
#5531=ADVANCED_FACE('',(#588),#5238,.T.);
#5532=ADVANCED_FACE('',(#589),#133,.T.);
#5533=ADVANCED_FACE('',(#590),#5239,.T.);
#5534=ADVANCED_FACE('',(#591),#134,.T.);
#5535=ADVANCED_FACE('',(#592),#5240,.T.);
#5536=ADVANCED_FACE('',(#593),#135,.T.);
#5537=ADVANCED_FACE('',(#594),#5241,.T.);
#5538=ADVANCED_FACE('',(#595),#5242,.T.);
#5539=ADVANCED_FACE('',(#596),#136,.T.);
#5540=ADVANCED_FACE('',(#597),#137,.T.);
#5541=ADVANCED_FACE('',(#598),#5243,.T.);
#5542=ADVANCED_FACE('',(#599),#138,.T.);
#5543=ADVANCED_FACE('',(#600),#5244,.T.);
#5544=ADVANCED_FACE('',(#601),#5245,.T.);
#5545=ADVANCED_FACE('',(#602),#5246,.T.);
#5546=ADVANCED_FACE('',(#603),#5247,.T.);
#5547=ADVANCED_FACE('',(#604),#5248,.T.);
#5548=ADVANCED_FACE('',(#605),#139,.T.);
#5549=ADVANCED_FACE('',(#606),#140,.T.);
#5550=ADVANCED_FACE('',(#607),#141,.T.);
#5551=ADVANCED_FACE('',(#608),#5249,.T.);
#5552=ADVANCED_FACE('',(#609),#142,.T.);
#5553=ADVANCED_FACE('',(#610),#5250,.T.);
#5554=ADVANCED_FACE('',(#611),#5251,.T.);
#5555=ADVANCED_FACE('',(#612),#5252,.T.);
#5556=ADVANCED_FACE('',(#613),#5253,.T.);
#5557=ADVANCED_FACE('',(#614),#5254,.T.);
#5558=ADVANCED_FACE('',(#615),#5255,.T.);
#5559=ADVANCED_FACE('',(#616),#223,.T.);
#5560=ADVANCED_FACE('',(#617),#5256,.T.);
#5561=ADVANCED_FACE('',(#618),#224,.T.);
#5562=ADVANCED_FACE('',(#619),#225,.T.);
#5563=ADVANCED_FACE('',(#620),#226,.T.);
#5564=ADVANCED_FACE('',(#621),#5257,.T.);
#5565=ADVANCED_FACE('',(#622),#5258,.T.);
#5566=ADVANCED_FACE('',(#623),#5259,.T.);
#5567=ADVANCED_FACE('',(#624),#5260,.T.);
#5568=ADVANCED_FACE('',(#625),#5261,.T.);
#5569=ADVANCED_FACE('',(#626),#5262,.F.);
#5570=ADVANCED_FACE('',(#627),#5263,.T.);
#5571=ADVANCED_FACE('',(#628),#5264,.F.);
#5572=ADVANCED_FACE('',(#629),#5265,.T.);
#5573=ADVANCED_FACE('',(#630),#5266,.T.);
#5574=ADVANCED_FACE('',(#631),#5267,.T.);
#5575=ADVANCED_FACE('',(#632),#5268,.T.);
#5576=ADVANCED_FACE('',(#633),#5269,.T.);
#5577=ADVANCED_FACE('',(#634),#5270,.T.);
#5578=ADVANCED_FACE('',(#635),#343,.F.);
#5579=ADVANCED_FACE('',(#636),#5271,.F.);
#5580=ADVANCED_FACE('',(#637),#5272,.F.);
#5581=ADVANCED_FACE('',(#638),#344,.T.);
#5582=ADVANCED_FACE('',(#639,#278,#279,#280,#281),#345,.F.);
#5583=ADVANCED_FACE('',(#640),#346,.F.);
#5584=ADVANCED_FACE('',(#641),#347,.T.);
#5585=ADVANCED_FACE('',(#642),#348,.F.);
#5586=ADVANCED_FACE('',(#643),#349,.F.);
#5587=ADVANCED_FACE('',(#644),#350,.F.);
#5588=ADVANCED_FACE('',(#645),#351,.F.);
#5589=ADVANCED_FACE('',(#646),#352,.F.);
#5590=ADVANCED_FACE('',(#647),#353,.F.);
#5591=ADVANCED_FACE('',(#648),#354,.F.);
#5592=ADVANCED_FACE('',(#649),#355,.F.);
#5593=ADVANCED_FACE('',(#650),#356,.T.);
#5716=CLOSED_SHELL('',(#5500,#5501,#5502,#5503,#5504,#5505,#5506,#5507,
#5508,#5509,#5510,#5511,#5512,#5513,#5514,#5515,#5516,#5517,#5518,#5519,
#5520,#5521,#5522,#5523,#5524,#5525,#5526,#5527,#5528,#5529,#5530,#5531,
#5532,#5533,#5534,#5535,#5536,#5537,#5538,#5539,#5540,#5541,#5542,#5543,
#5544,#5545,#5546,#5547,#5548,#5549,#5550,#5551,#5552,#5553,#5554,#5555,
#5556,#5557,#5558,#5559,#5560,#5561,#5562,#5563,#5564,#5565,#5566,#5567,
#5568,#5569,#5570,#5571,#5572,#5573,#5574,#5575,#5576,#5577,#5578,#5579,
#5580,#5581,#5582,#5583,#5584,#5585,#5586,#5587,#5588,#5589,#5590,#5591,
#5592,#5593));
#6224=AXIS2_PLACEMENT_3D('',#9495,#7623,#7624);
#6225=AXIS2_PLACEMENT_3D('',#9496,#7625,#7626);
#6226=AXIS2_PLACEMENT_3D('',#9498,#7627,#7628);
#6227=AXIS2_PLACEMENT_3D('',#9500,#7629,#7630);
#6228=AXIS2_PLACEMENT_3D('',#9501,#7631,#7632);
#6229=AXIS2_PLACEMENT_3D('',#9502,#7633,#7634);
#6230=AXIS2_PLACEMENT_3D('',#9512,#7639,#7640);
#6231=AXIS2_PLACEMENT_3D('',#9513,#7641,#7642);
#6232=AXIS2_PLACEMENT_3D('',#9516,#7644,#7645);
#6233=AXIS2_PLACEMENT_3D('',#9517,#7646,#7647);
#6234=AXIS2_PLACEMENT_3D('',#9519,#7648,#7649);
#6235=AXIS2_PLACEMENT_3D('',#9520,#7650,#7651);
#6236=AXIS2_PLACEMENT_3D('',#9521,#7652,#7653);
#6237=AXIS2_PLACEMENT_3D('',#9524,#7655,#7656);
#6238=AXIS2_PLACEMENT_3D('',#9525,#7657,#7658);
#6239=AXIS2_PLACEMENT_3D('',#9527,#7659,#7660);
#6240=AXIS2_PLACEMENT_3D('',#9529,#7661,#7662);
#6241=AXIS2_PLACEMENT_3D('',#9531,#7663,#7664);
#6242=AXIS2_PLACEMENT_3D('',#9532,#7665,#7666);
#6243=AXIS2_PLACEMENT_3D('',#9533,#7667,#7668);
#6244=AXIS2_PLACEMENT_3D('',#9543,#7673,#7674);
#6245=AXIS2_PLACEMENT_3D('',#9544,#7675,#7676);
#6246=AXIS2_PLACEMENT_3D('',#9547,#7678,#7679);
#6247=AXIS2_PLACEMENT_3D('',#9548,#7680,#7681);
#6248=AXIS2_PLACEMENT_3D('',#9550,#7682,#7683);
#6249=AXIS2_PLACEMENT_3D('',#9552,#7684,#7685);
#6250=AXIS2_PLACEMENT_3D('',#9553,#7686,#7687);
#6251=AXIS2_PLACEMENT_3D('',#9554,#7688,#7689);
#6252=AXIS2_PLACEMENT_3D('',#9557,#7691,#7692);
#6253=AXIS2_PLACEMENT_3D('',#9558,#7693,#7694);
#6254=AXIS2_PLACEMENT_3D('',#9561,#7695,#7696);
#6255=AXIS2_PLACEMENT_3D('',#9563,#7697,#7698);
#6256=AXIS2_PLACEMENT_3D('',#9564,#7699,#7700);
#6257=AXIS2_PLACEMENT_3D('',#9565,#7701,#7702);
#6258=AXIS2_PLACEMENT_3D('',#9568,#7703,#7704);
#6259=AXIS2_PLACEMENT_3D('',#9570,#7705,#7706);
#6260=AXIS2_PLACEMENT_3D('',#9571,#7707,#7708);
#6261=AXIS2_PLACEMENT_3D('',#9572,#7709,#7710);
#6262=AXIS2_PLACEMENT_3D('',#9575,#7711,#7712);
#6263=AXIS2_PLACEMENT_3D('',#9577,#7713,#7714);
#6264=AXIS2_PLACEMENT_3D('',#9578,#7715,#7716);
#6265=AXIS2_PLACEMENT_3D('',#9579,#7717,#7718);
#6266=AXIS2_PLACEMENT_3D('',#9582,#7721,#7722);
#6267=AXIS2_PLACEMENT_3D('',#9584,#7723,#7724);
#6268=AXIS2_PLACEMENT_3D('',#9586,#7725,#7726);
#6269=AXIS2_PLACEMENT_3D('',#9587,#7727,#7728);
#6270=AXIS2_PLACEMENT_3D('',#9588,#7729,#7730);
#6271=AXIS2_PLACEMENT_3D('',#9591,#7733,#7734);
#6272=AXIS2_PLACEMENT_3D('',#9594,#7735,#7736);
#6273=AXIS2_PLACEMENT_3D('',#9596,#7737,#7738);
#6274=AXIS2_PLACEMENT_3D('',#9597,#7739,#7740);
#6275=AXIS2_PLACEMENT_3D('',#9598,#7741,#7742);
#6276=AXIS2_PLACEMENT_3D('',#9601,#7745,#7746);
#6277=AXIS2_PLACEMENT_3D('',#9604,#7749,#7750);
#6278=AXIS2_PLACEMENT_3D('',#9606,#7751,#7752);
#6279=AXIS2_PLACEMENT_3D('',#9608,#7753,#7754);
#6280=AXIS2_PLACEMENT_3D('',#9609,#7755,#7756);
#6281=AXIS2_PLACEMENT_3D('',#9610,#7757,#7758);
#6282=AXIS2_PLACEMENT_3D('',#9613,#7761,#7762);
#6283=AXIS2_PLACEMENT_3D('',#9616,#7763,#7764);
#6284=AXIS2_PLACEMENT_3D('',#9617,#7765,#7766);
#6285=AXIS2_PLACEMENT_3D('',#9618,#7767,#7768);
#6286=AXIS2_PLACEMENT_3D('',#9619,#7769,#7770);
#6287=AXIS2_PLACEMENT_3D('',#9621,#7771,#7772);
#6288=AXIS2_PLACEMENT_3D('',#9623,#7773,#7774);
#6289=AXIS2_PLACEMENT_3D('',#9625,#7775,#7776);
#6290=AXIS2_PLACEMENT_3D('',#9626,#7777,#7778);
#6291=AXIS2_PLACEMENT_3D('',#9627,#7779,#7780);
#6292=AXIS2_PLACEMENT_3D('',#9630,#7781,#7782);
#6293=AXIS2_PLACEMENT_3D('',#9631,#7783,#7784);
#6294=AXIS2_PLACEMENT_3D('',#9632,#7785,#7786);
#6295=AXIS2_PLACEMENT_3D('',#9633,#7787,#7788);
#6296=AXIS2_PLACEMENT_3D('',#9635,#7790,#7791);
#6297=AXIS2_PLACEMENT_3D('',#9638,#7792,#7793);
#6298=AXIS2_PLACEMENT_3D('',#9639,#7794,#7795);
#6299=AXIS2_PLACEMENT_3D('',#9641,#7796,#7797);
#6300=AXIS2_PLACEMENT_3D('',#9642,#7798,#7799);
#6301=AXIS2_PLACEMENT_3D('',#9643,#7800,#7801);
#6302=AXIS2_PLACEMENT_3D('',#9646,#7802,#7803);
#6303=AXIS2_PLACEMENT_3D('',#9647,#7804,#7805);
#6304=AXIS2_PLACEMENT_3D('',#9649,#7806,#7807);
#6305=AXIS2_PLACEMENT_3D('',#9650,#7808,#7809);
#6306=AXIS2_PLACEMENT_3D('',#9651,#7810,#7811);
#6307=AXIS2_PLACEMENT_3D('',#9654,#7812,#7813);
#6308=AXIS2_PLACEMENT_3D('',#9656,#7814,#7815);
#6309=AXIS2_PLACEMENT_3D('',#9657,#7816,#7817);
#6310=AXIS2_PLACEMENT_3D('',#9658,#7818,#7819);
#6311=AXIS2_PLACEMENT_3D('',#9661,#7822,#7823);
#6312=AXIS2_PLACEMENT_3D('',#9663,#7824,#7825);
#6313=AXIS2_PLACEMENT_3D('',#9665,#7826,#7827);
#6314=AXIS2_PLACEMENT_3D('',#9667,#7828,#7829);
#6315=AXIS2_PLACEMENT_3D('',#9668,#7830,#7831);
#6316=AXIS2_PLACEMENT_3D('',#9669,#7832,#7833);
#6317=AXIS2_PLACEMENT_3D('',#9672,#7834,#7835);
#6318=AXIS2_PLACEMENT_3D('',#9674,#7836,#7837);
#6319=AXIS2_PLACEMENT_3D('',#9675,#7838,#7839);
#6320=AXIS2_PLACEMENT_3D('',#9676,#7840,#7841);
#6321=AXIS2_PLACEMENT_3D('',#9679,#7844,#7845);
#6322=AXIS2_PLACEMENT_3D('',#9682,#7846,#7847);
#6323=AXIS2_PLACEMENT_3D('',#9684,#7848,#7849);
#6324=AXIS2_PLACEMENT_3D('',#9685,#7850,#7851);
#6325=AXIS2_PLACEMENT_3D('',#9686,#7852,#7853);
#6326=AXIS2_PLACEMENT_3D('',#9689,#7856,#7857);
#6327=AXIS2_PLACEMENT_3D('',#9692,#7858,#7859);
#6328=AXIS2_PLACEMENT_3D('',#9694,#7860,#7861);
#6329=AXIS2_PLACEMENT_3D('',#9695,#7862,#7863);
#6330=AXIS2_PLACEMENT_3D('',#9696,#7864,#7865);
#6331=AXIS2_PLACEMENT_3D('',#9699,#7868,#7869);
#6332=AXIS2_PLACEMENT_3D('',#9702,#7870,#7871);
#6333=AXIS2_PLACEMENT_3D('',#9704,#7872,#7873);
#6334=AXIS2_PLACEMENT_3D('',#9705,#7874,#7875);
#6335=AXIS2_PLACEMENT_3D('',#9706,#7876,#7877);
#6336=AXIS2_PLACEMENT_3D('',#9709,#7880,#7881);
#6337=AXIS2_PLACEMENT_3D('',#9712,#7884,#7885);
#6338=AXIS2_PLACEMENT_3D('',#9715,#7886,#7887);
#6339=AXIS2_PLACEMENT_3D('',#9717,#7888,#7889);
#6340=AXIS2_PLACEMENT_3D('',#9718,#7890,#7891);
#6341=AXIS2_PLACEMENT_3D('',#9719,#7892,#7893);
#6342=AXIS2_PLACEMENT_3D('',#9722,#7894,#7895);
#6343=AXIS2_PLACEMENT_3D('',#9724,#7896,#7897);
#6344=AXIS2_PLACEMENT_3D('',#9725,#7898,#7899);
#6345=AXIS2_PLACEMENT_3D('',#9726,#7900,#7901);
#6346=AXIS2_PLACEMENT_3D('',#9745,#7904,#7905);
#6347=AXIS2_PLACEMENT_3D('',#9748,#7906,#7907);
#6348=AXIS2_PLACEMENT_3D('',#9750,#7908,#7909);
#6349=AXIS2_PLACEMENT_3D('',#9751,#7910,#7911);
#6350=AXIS2_PLACEMENT_3D('',#9752,#7912,#7913);
#6351=AXIS2_PLACEMENT_3D('',#9755,#7916,#7917);
#6352=AXIS2_PLACEMENT_3D('',#9758,#7920,#7921);
#6353=AXIS2_PLACEMENT_3D('',#9777,#7924,#7925);
#6354=AXIS2_PLACEMENT_3D('',#9796,#7928,#7929);
#6355=AXIS2_PLACEMENT_3D('',#9815,#7932,#7933);
#6356=AXIS2_PLACEMENT_3D('',#9818,#7934,#7935);
#6357=AXIS2_PLACEMENT_3D('',#9820,#7936,#7937);
#6358=AXIS2_PLACEMENT_3D('',#9821,#7938,#7939);
#6359=AXIS2_PLACEMENT_3D('',#9822,#7940,#7941);
#6360=AXIS2_PLACEMENT_3D('',#9825,#7942,#7943);
#6361=AXIS2_PLACEMENT_3D('',#9827,#7944,#7945);
#6362=AXIS2_PLACEMENT_3D('',#9828,#7946,#7947);
#6363=AXIS2_PLACEMENT_3D('',#9829,#7948,#7949);
#6364=AXIS2_PLACEMENT_3D('',#9832,#7950,#7951);
#6365=AXIS2_PLACEMENT_3D('',#9834,#7952,#7953);
#6366=AXIS2_PLACEMENT_3D('',#9835,#7954,#7955);
#6367=AXIS2_PLACEMENT_3D('',#9836,#7956,#7957);
#6368=AXIS2_PLACEMENT_3D('',#9839,#7960,#7961);
#6369=AXIS2_PLACEMENT_3D('',#9842,#7962,#7963);
#6370=AXIS2_PLACEMENT_3D('',#9844,#7964,#7965);
#6371=AXIS2_PLACEMENT_3D('',#9845,#7966,#7967);
#6372=AXIS2_PLACEMENT_3D('',#9846,#7968,#7969);
#6373=AXIS2_PLACEMENT_3D('',#9865,#7972,#7973);
#6374=AXIS2_PLACEMENT_3D('',#9868,#7976,#7977);
#6375=AXIS2_PLACEMENT_3D('',#9871,#7980,#7981);
#6376=AXIS2_PLACEMENT_3D('',#9890,#7984,#7985);
#6377=AXIS2_PLACEMENT_3D('',#9893,#7988,#7989);
#6378=AXIS2_PLACEMENT_3D('',#9912,#7992,#7993);
#6379=AXIS2_PLACEMENT_3D('',#9913,#7994,#7995);
#6380=AXIS2_PLACEMENT_3D('',#9914,#7996,#7997);
#6381=AXIS2_PLACEMENT_3D('',#9915,#7998,#7999);
#6382=AXIS2_PLACEMENT_3D('',#9934,#8002,#8003);
#6383=AXIS2_PLACEMENT_3D('',#9935,#8004,#8005);
#6384=AXIS2_PLACEMENT_3D('',#9936,#8006,#8007);
#6385=AXIS2_PLACEMENT_3D('',#9937,#8008,#8009);
#6386=AXIS2_PLACEMENT_3D('',#9938,#8010,#8011);
#6387=AXIS2_PLACEMENT_3D('',#9939,#8012,#8013);
#6388=AXIS2_PLACEMENT_3D('',#9940,#8014,#8015);
#6389=AXIS2_PLACEMENT_3D('',#9941,#8016,#8017);
#6390=AXIS2_PLACEMENT_3D('',#9942,#8018,#8019);
#6391=AXIS2_PLACEMENT_3D('',#9943,#8020,#8021);
#6392=AXIS2_PLACEMENT_3D('',#9946,#8024,#8025);
#6393=AXIS2_PLACEMENT_3D('',#9949,#8028,#8029);
#6394=AXIS2_PLACEMENT_3D('',#9952,#8032,#8033);
#6395=AXIS2_PLACEMENT_3D('',#9955,#8036,#8037);
#6396=AXIS2_PLACEMENT_3D('',#9957,#8039,#8040);
#6397=AXIS2_PLACEMENT_3D('',#9959,#8042,#8043);
#6398=AXIS2_PLACEMENT_3D('',#9961,#8045,#8046);
#6399=AXIS2_PLACEMENT_3D('',#9963,#8048,#8049);
#6400=AXIS2_PLACEMENT_3D('',#9965,#8051,#8052);
#6401=AXIS2_PLACEMENT_3D('',#9968,#8055,#8056);
#6402=AXIS2_PLACEMENT_3D('',#9970,#8058,#8059);
#6403=AXIS2_PLACEMENT_3D('',#9973,#8062,#8063);
#6404=AXIS2_PLACEMENT_3D('',#9975,#8065,#8066);
#6405=AXIS2_PLACEMENT_3D('',#9978,#8069,#8070);
#6406=AXIS2_PLACEMENT_3D('',#9980,#8072,#8073);
#6407=AXIS2_PLACEMENT_3D('',#9982,#8075,#8076);
#6408=AXIS2_PLACEMENT_3D('',#9985,#8079,#8080);
#6409=AXIS2_PLACEMENT_3D('',#9986,#8081,#8082);
#6410=AXIS2_PLACEMENT_3D('',#9987,#8083,#8084);
#6411=AXIS2_PLACEMENT_3D('',#9988,#8085,#8086);
#6412=AXIS2_PLACEMENT_3D('',#9989,#8087,#8088);
#6413=AXIS2_PLACEMENT_3D('',#9990,#8089,#8090);
#6414=AXIS2_PLACEMENT_3D('',#9991,#8091,#8092);
#6415=AXIS2_PLACEMENT_3D('',#9992,#8093,#8094);
#6416=AXIS2_PLACEMENT_3D('',#9993,#8095,#8096);
#6417=AXIS2_PLACEMENT_3D('',#9994,#8097,#8098);
#6418=AXIS2_PLACEMENT_3D('',#9995,#8099,#8100);
#6419=AXIS2_PLACEMENT_3D('',#9996,#8101,#8102);
#6420=AXIS2_PLACEMENT_3D('',#9997,#8103,#8104);
#7623=DIRECTION('axis',(0.,0.,1.));
#7624=DIRECTION('refdir',(1.,0.,0.));
#7625=DIRECTION('center_axis',(0.,0.,1.));
#7626=DIRECTION('ref_axis',(-1.,0.,0.));
#7627=DIRECTION('center_axis',(0.,0.,1.));
#7628=DIRECTION('ref_axis',(-1.,0.,0.));
#7629=DIRECTION('center_axis',(0.,1.,0.));
#7630=DIRECTION('ref_axis',(1.,0.,0.));
#7631=DIRECTION('center_axis',(0.,0.,-1.));
#7632=DIRECTION('ref_axis',(-1.,0.,0.));
#7633=DIRECTION('center_axis',(0.,0.,-1.));
#7634=DIRECTION('ref_axis',(-1.,0.,0.));
#7635=DIRECTION('',(-1.,0.,0.));
#7636=DIRECTION('',(0.,-1.,0.));
#7637=DIRECTION('',(1.,-2.77555756156289E-16,0.));
#7638=DIRECTION('',(5.9211894646675E-16,1.,0.));
#7639=DIRECTION('center_axis',(0.,0.,-1.));
#7640=DIRECTION('ref_axis',(-1.,0.,0.));
#7641=DIRECTION('center_axis',(0.,0.,1.));
#7642=DIRECTION('ref_axis',(-1.,0.,0.));
#7643=DIRECTION('',(0.,0.,-1.));
#7644=DIRECTION('center_axis',(0.,0.,1.));
#7645=DIRECTION('ref_axis',(-1.,0.,0.));
#7646=DIRECTION('center_axis',(0.,0.,1.));
#7647=DIRECTION('ref_axis',(-1.,0.,0.));
#7648=DIRECTION('center_axis',(0.,0.,1.));
#7649=DIRECTION('ref_axis',(-1.,0.,0.));
#7650=DIRECTION('center_axis',(0.,1.,0.));
#7651=DIRECTION('ref_axis',(1.,0.,0.));
#7652=DIRECTION('center_axis',(0.,0.,1.));
#7653=DIRECTION('ref_axis',(-1.,0.,0.));
#7654=DIRECTION('',(0.,0.,-1.));
#7655=DIRECTION('center_axis',(0.,0.,1.));
#7656=DIRECTION('ref_axis',(-1.,0.,0.));
#7657=DIRECTION('center_axis',(0.,0.,-1.));
#7658=DIRECTION('ref_axis',(1.,0.,0.));
#7659=DIRECTION('center_axis',(0.,0.,-1.));
#7660=DIRECTION('ref_axis',(-1.,0.,0.));
#7661=DIRECTION('center_axis',(0.,1.,0.));
#7662=DIRECTION('ref_axis',(-1.,0.,0.));
#7663=DIRECTION('center_axis',(0.,0.,1.));
#7664=DIRECTION('ref_axis',(-1.,0.,0.));
#7665=DIRECTION('center_axis',(0.,0.,1.));
#7666=DIRECTION('ref_axis',(-1.,0.,0.));
#7667=DIRECTION('center_axis',(0.,0.,1.));
#7668=DIRECTION('ref_axis',(-1.,0.,0.));
#7669=DIRECTION('',(-1.,0.,0.));
#7670=DIRECTION('',(0.,-1.,0.));
#7671=DIRECTION('',(1.,0.,0.));
#7672=DIRECTION('',(5.9211894646675E-16,1.,0.));
#7673=DIRECTION('center_axis',(0.,0.,-1.));
#7674=DIRECTION('ref_axis',(-1.,0.,0.));
#7675=DIRECTION('center_axis',(0.,0.,-1.));
#7676=DIRECTION('ref_axis',(-1.,0.,0.));
#7677=DIRECTION('',(0.,0.,-1.));
#7678=DIRECTION('center_axis',(0.,0.,-1.));
#7679=DIRECTION('ref_axis',(-1.,0.,0.));
#7680=DIRECTION('center_axis',(0.,0.,-1.));
#7681=DIRECTION('ref_axis',(1.,0.,0.));
#7682=DIRECTION('center_axis',(0.,1.,0.));
#7683=DIRECTION('ref_axis',(-1.,0.,0.));
#7684=DIRECTION('center_axis',(0.,0.,1.));
#7685=DIRECTION('ref_axis',(-1.,0.,0.));
#7686=DIRECTION('center_axis',(0.,0.,1.));
#7687=DIRECTION('ref_axis',(-1.,0.,0.));
#7688=DIRECTION('center_axis',(0.,0.,-1.));
#7689=DIRECTION('ref_axis',(-1.,0.,0.));
#7690=DIRECTION('',(0.,0.,-1.));
#7691=DIRECTION('center_axis',(0.,0.,-1.));
#7692=DIRECTION('ref_axis',(-1.,0.,0.));
#7693=DIRECTION('center_axis',(-0.408248290463861,0.408248290463837,-0.81649658092774));
#7694=DIRECTION('ref_axis',(0.577350269189669,-0.577350269189598,-0.57735026918961));
#7695=DIRECTION('center_axis',(0.,7.40148683083442E-15,1.));
#7696=DIRECTION('ref_axis',(1.,0.,0.));
#7697=DIRECTION('center_axis',(-1.,0.,5.92118946466745E-14));
#7698=DIRECTION('ref_axis',(0.,-1.,0.));
#7699=DIRECTION('center_axis',(0.,1.,0.));
#7700=DIRECTION('ref_axis',(0.,0.,-1.));
#7701=DIRECTION('center_axis',(0.408248290463865,-0.81649658092773,0.408248290463853));
#7702=DIRECTION('ref_axis',(-0.577350269189602,-0.577350269189626,-0.577350269189649));
#7703=DIRECTION('center_axis',(1.,0.,0.));
#7704=DIRECTION('ref_axis',(0.,0.,-1.));
#7705=DIRECTION('center_axis',(-7.40148683083454E-15,0.,1.));
#7706=DIRECTION('ref_axis',(0.,-1.,0.));
#7707=DIRECTION('center_axis',(0.,1.,2.96059473233375E-14));
#7708=DIRECTION('ref_axis',(-1.,0.,0.));
#7709=DIRECTION('center_axis',(0.816496580927716,-0.408248290463882,0.408248290463864));
#7710=DIRECTION('ref_axis',(0.577350269189634,0.577350269189634,-0.57735026918961));
#7711=DIRECTION('center_axis',(-1.,0.,0.));
#7712=DIRECTION('ref_axis',(0.,0.,-1.));
#7713=DIRECTION('center_axis',(0.,0.,1.));
#7714=DIRECTION('ref_axis',(0.,1.,0.));
#7715=DIRECTION('center_axis',(0.,-1.,0.));
#7716=DIRECTION('ref_axis',(1.,0.,0.));
#7717=DIRECTION('center_axis',(-5.9211894646675E-16,-1.,0.));
#7718=DIRECTION('ref_axis',(0.707106781186563,0.,-0.707106781186532));
#7719=DIRECTION('',(5.9211894646675E-16,1.,0.));
#7720=DIRECTION('',(-5.9211894646675E-16,-1.,0.));
#7721=DIRECTION('center_axis',(0.816496580927728,0.408248290463864,-0.408248290463858));
#7722=DIRECTION('ref_axis',(0.577350269189594,-0.577350269189642,0.577350269189642));
#7723=DIRECTION('center_axis',(0.,1.,0.));
#7724=DIRECTION('ref_axis',(1.,0.,0.));
#7725=DIRECTION('center_axis',(-1.,0.,0.));
#7726=DIRECTION('ref_axis',(0.,0.,1.));
#7727=DIRECTION('center_axis',(-7.40148683083454E-15,0.,-1.));
#7728=DIRECTION('ref_axis',(0.,-1.,0.));
#7729=DIRECTION('center_axis',(0.,0.,-1.));
#7730=DIRECTION('ref_axis',(0.707106781186516,-0.707106781186579,0.));
#7731=DIRECTION('',(0.,0.,1.));
#7732=DIRECTION('',(0.,0.,-1.));
#7733=DIRECTION('center_axis',(-0.408248290463855,-0.816496580927734,-0.408248290463855));
#7734=DIRECTION('ref_axis',(-0.577350269189651,0.577350269189604,-0.577350269189622));
#7735=DIRECTION('center_axis',(0.,0.,1.));
#7736=DIRECTION('ref_axis',(-1.,0.,0.));
#7737=DIRECTION('center_axis',(1.,0.,0.));
#7738=DIRECTION('ref_axis',(0.,1.,0.));
#7739=DIRECTION('center_axis',(0.,-1.,0.));
#7740=DIRECTION('ref_axis',(0.,0.,-1.));
#7741=DIRECTION('center_axis',(0.,-1.,0.));
#7742=DIRECTION('ref_axis',(-0.707106781186563,0.,-0.707106781186532));
#7743=DIRECTION('',(0.,1.,0.));
#7744=DIRECTION('',(0.,-1.,0.));
#7745=DIRECTION('center_axis',(-1.,0.,0.));
#7746=DIRECTION('ref_axis',(0.,0.707106781186553,-0.707106781186542));
#7747=DIRECTION('',(1.,0.,0.));
#7748=DIRECTION('',(-1.,0.,0.));
#7749=DIRECTION('center_axis',(0.408248290463864,-0.816496580927728,-0.408248290463858));
#7750=DIRECTION('ref_axis',(-0.5773502691896,-0.577350269189624,0.577350269189653));
#7751=DIRECTION('center_axis',(1.,0.,0.));
#7752=DIRECTION('ref_axis',(0.,-1.,0.));
#7753=DIRECTION('center_axis',(-1.48029736616691E-14,1.,0.));
#7754=DIRECTION('ref_axis',(0.,0.,1.));
#7755=DIRECTION('center_axis',(0.,-7.40148683083454E-15,-1.));
#7756=DIRECTION('ref_axis',(-1.,0.,0.));
#7757=DIRECTION('center_axis',(0.,0.,-1.));
#7758=DIRECTION('ref_axis',(-0.707106781186568,-0.707106781186527,0.));
#7759=DIRECTION('',(0.,0.,1.));
#7760=DIRECTION('',(0.,0.,-1.));
#7761=DIRECTION('center_axis',(0.408248290463856,-0.816496580927712,0.408248290463898));
#7762=DIRECTION('ref_axis',(0.577350269189574,0.577350269189645,0.577350269189657));
#7763=DIRECTION('center_axis',(0.,0.,-1.));
#7764=DIRECTION('ref_axis',(1.,0.,0.));
#7765=DIRECTION('center_axis',(-1.,0.,5.9211894646675E-14));
#7766=DIRECTION('ref_axis',(0.,1.,0.));
#7767=DIRECTION('center_axis',(-1.48029736616699E-14,-1.,0.));
#7768=DIRECTION('ref_axis',(0.,0.,1.));
#7769=DIRECTION('center_axis',(-1.,0.,0.));
#7770=DIRECTION('ref_axis',(0.,0.,-1.));
#7771=DIRECTION('center_axis',(1.,0.,0.));
#7772=DIRECTION('ref_axis',(0.,1.,0.));
#7773=DIRECTION('center_axis',(0.,1.,0.));
#7774=DIRECTION('ref_axis',(0.,0.,1.));
#7775=DIRECTION('center_axis',(-1.,5.9211894646675E-16,0.));
#7776=DIRECTION('ref_axis',(0.,0.707106781186545,-0.70710678118655));
#7777=DIRECTION('center_axis',(0.,0.,-1.));
#7778=DIRECTION('ref_axis',(1.,0.,0.));
#7779=DIRECTION('center_axis',(-0.408248290463862,-0.816496580927724,0.408248290463868));
#7780=DIRECTION('ref_axis',(-0.57735026918959,0.577350269189638,0.577350269189649));
#7781=DIRECTION('center_axis',(0.,0.,-1.));
#7782=DIRECTION('ref_axis',(0.,1.,0.));
#7783=DIRECTION('center_axis',(0.,-1.,0.));
#7784=DIRECTION('ref_axis',(-1.,0.,0.));
#7785=DIRECTION('center_axis',(1.,0.,0.));
#7786=DIRECTION('ref_axis',(0.,0.,1.));
#7787=DIRECTION('center_axis',(1.,0.,0.));
#7788=DIRECTION('ref_axis',(0.,0.707106781186542,0.707106781186553));
#7789=DIRECTION('',(1.,0.,0.));
#7790=DIRECTION('center_axis',(-1.,0.,0.));
#7791=DIRECTION('ref_axis',(0.,0.,-1.));
#7792=DIRECTION('center_axis',(1.,0.,0.));
#7793=DIRECTION('ref_axis',(0.,0.707106781186545,-0.70710678118655));
#7794=DIRECTION('center_axis',(0.,1.,0.));
#7795=DIRECTION('ref_axis',(-1.,0.,0.));
#7796=DIRECTION('center_axis',(-1.,0.,0.));
#7797=DIRECTION('ref_axis',(0.,0.,-1.));
#7798=DIRECTION('center_axis',(0.,0.,-1.));
#7799=DIRECTION('ref_axis',(0.,-1.,0.));
#7800=DIRECTION('center_axis',(1.,0.,0.));
#7801=DIRECTION('ref_axis',(0.,0.,1.));
#7802=DIRECTION('center_axis',(-1.,5.9211894646675E-16,0.));
#7803=DIRECTION('ref_axis',(0.,-0.70710678118654,-0.707106781186555));
#7804=DIRECTION('center_axis',(0.,-1.,0.));
#7805=DIRECTION('ref_axis',(1.,0.,0.));
#7806=DIRECTION('center_axis',(1.,-5.92118946466763E-14,0.));
#7807=DIRECTION('ref_axis',(0.,0.,-1.));
#7808=DIRECTION('center_axis',(0.,0.,-1.));
#7809=DIRECTION('ref_axis',(0.,1.,0.));
#7810=DIRECTION('center_axis',(-0.408248290463862,-0.816496580927724,-0.408248290463868));
#7811=DIRECTION('ref_axis',(0.577350269189592,-0.577350269189639,0.577350269189645));
#7812=DIRECTION('center_axis',(0.,1.,0.));
#7813=DIRECTION('ref_axis',(1.,0.,0.));
#7814=DIRECTION('center_axis',(-1.,-5.92118946466754E-14,0.));
#7815=DIRECTION('ref_axis',(0.,0.,1.));
#7816=DIRECTION('center_axis',(0.,0.,-1.));
#7817=DIRECTION('ref_axis',(0.,-1.,0.));
#7818=DIRECTION('center_axis',(0.,0.,1.));
#7819=DIRECTION('ref_axis',(0.707106781186527,-0.707106781186568,0.));
#7820=DIRECTION('',(0.,0.,-1.));
#7821=DIRECTION('',(0.,0.,1.));
#7822=DIRECTION('center_axis',(1.,0.,0.));
#7823=DIRECTION('ref_axis',(0.,0.,1.));
#7824=DIRECTION('center_axis',(-1.,0.,0.));
#7825=DIRECTION('ref_axis',(0.,-1.,0.));
#7826=DIRECTION('center_axis',(0.,-1.,0.));
#7827=DIRECTION('ref_axis',(0.,0.,1.));
#7828=DIRECTION('center_axis',(1.,0.,0.));
#7829=DIRECTION('ref_axis',(0.,-0.70710678118654,-0.707106781186555));
#7830=DIRECTION('center_axis',(0.,0.,-1.));
#7831=DIRECTION('ref_axis',(-1.,0.,0.));
#7832=DIRECTION('center_axis',(0.408248290463867,-0.816496580927722,-0.408248290463867));
#7833=DIRECTION('ref_axis',(-0.5773502691896,-0.577350269189636,0.577350269189642));
#7834=DIRECTION('center_axis',(1.,0.,0.));
#7835=DIRECTION('ref_axis',(0.,-1.,0.));
#7836=DIRECTION('center_axis',(0.,1.,0.));
#7837=DIRECTION('ref_axis',(0.,0.,1.));
#7838=DIRECTION('center_axis',(0.,0.,-1.));
#7839=DIRECTION('ref_axis',(-1.,0.,0.));
#7840=DIRECTION('center_axis',(0.,0.,-1.));
#7841=DIRECTION('ref_axis',(-0.707106781186568,-0.707106781186527,0.));
#7842=DIRECTION('',(0.,0.,1.));
#7843=DIRECTION('',(0.,0.,-1.));
#7844=DIRECTION('center_axis',(0.408248290463866,-0.81649658092772,0.408248290463872));
#7845=DIRECTION('ref_axis',(0.577350269189592,0.577350269189628,0.577350269189657));
#7846=DIRECTION('center_axis',(-1.,0.,-5.9211894646675E-14));
#7847=DIRECTION('ref_axis',(0.,1.,0.));
#7848=DIRECTION('center_axis',(1.48029736616682E-14,-1.,0.));
#7849=DIRECTION('ref_axis',(0.,0.,1.));
#7850=DIRECTION('center_axis',(0.,0.,-1.));
#7851=DIRECTION('ref_axis',(1.,0.,0.));
#7852=DIRECTION('center_axis',(0.,0.,-1.));
#7853=DIRECTION('ref_axis',(0.707106781186527,0.707106781186568,0.));
#7854=DIRECTION('',(0.,0.,1.));
#7855=DIRECTION('',(0.,0.,-1.));
#7856=DIRECTION('center_axis',(0.408248290463859,0.408248290463847,-0.816496580927736));
#7857=DIRECTION('ref_axis',(0.577350269189657,0.577350269189622,0.577350269189598));
#7858=DIRECTION('center_axis',(0.,-7.40148683083442E-15,-1.));
#7859=DIRECTION('ref_axis',(1.,0.,0.));
#7860=DIRECTION('center_axis',(-1.,0.,0.));
#7861=DIRECTION('ref_axis',(0.,1.,0.));
#7862=DIRECTION('center_axis',(0.,-1.,0.));
#7863=DIRECTION('ref_axis',(0.,0.,1.));
#7864=DIRECTION('center_axis',(5.9211894646675E-16,1.,0.));
#7865=DIRECTION('ref_axis',(0.707106781186563,0.,0.707106781186532));
#7866=DIRECTION('',(-5.9211894646675E-16,-1.,0.));
#7867=DIRECTION('',(5.9211894646675E-16,1.,0.));
#7868=DIRECTION('center_axis',(-0.408248290463865,-0.81649658092773,0.408248290463853));
#7869=DIRECTION('ref_axis',(-0.5773502691896,0.577350269189624,0.577350269189653));
#7870=DIRECTION('center_axis',(0.,-1.,-2.96059473233375E-14));
#7871=DIRECTION('ref_axis',(-1.,0.,0.));
#7872=DIRECTION('center_axis',(1.,0.,0.));
#7873=DIRECTION('ref_axis',(0.,0.,1.));
#7874=DIRECTION('center_axis',(0.,0.,-1.));
#7875=DIRECTION('ref_axis',(0.,1.,0.));
#7876=DIRECTION('center_axis',(0.,0.,-1.));
#7877=DIRECTION('ref_axis',(-0.707106781186568,0.707106781186527,0.));
#7878=DIRECTION('',(0.,0.,1.));
#7879=DIRECTION('',(0.,0.,-1.));
#7880=DIRECTION('center_axis',(-1.,2.77555756156289E-16,0.));
#7881=DIRECTION('ref_axis',(0.,0.707106781186553,0.707106781186542));
#7882=DIRECTION('',(1.,-2.77555756156289E-16,0.));
#7883=DIRECTION('',(-1.,2.77555756156289E-16,0.));
#7884=DIRECTION('center_axis',(-0.408248290463862,-0.816496580927724,0.408248290463868));
#7885=DIRECTION('ref_axis',(-0.57735026918959,0.577350269189638,0.577350269189649));
#7886=DIRECTION('center_axis',(0.,-1.,0.));
#7887=DIRECTION('ref_axis',(-1.,0.,0.));
#7888=DIRECTION('center_axis',(1.,0.,0.));
#7889=DIRECTION('ref_axis',(0.,0.,1.));
#7890=DIRECTION('center_axis',(-7.40148683083454E-15,0.,-1.));
#7891=DIRECTION('ref_axis',(0.,1.,0.));
#7892=DIRECTION('center_axis',(0.408248290463859,-0.408248290463835,-0.816496580927742));
#7893=DIRECTION('ref_axis',(0.577350269189663,-0.577350269189604,0.57735026918961));
#7894=DIRECTION('center_axis',(7.40148683083454E-15,0.,-1.));
#7895=DIRECTION('ref_axis',(0.,-1.,0.));
#7896=DIRECTION('center_axis',(0.,1.,0.));
#7897=DIRECTION('ref_axis',(1.,0.,0.));
#7898=DIRECTION('center_axis',(-1.,-5.92118946466754E-14,0.));
#7899=DIRECTION('ref_axis',(0.,0.,1.));
#7900=DIRECTION('center_axis',(0.,0.,1.));
#7901=DIRECTION('ref_axis',(0.707106781186516,0.707106781186579,0.));
#7902=DIRECTION('',(0.,0.,1.));
#7903=DIRECTION('',(0.,0.,-1.));
#7904=DIRECTION('center_axis',(0.816496580927732,-0.408248290463866,0.408248290463848));
#7905=DIRECTION('ref_axis',(-0.577350269189588,-0.577350269189659,0.57735026918963));
#7906=DIRECTION('center_axis',(0.,7.40148683083454E-15,-1.));
#7907=DIRECTION('ref_axis',(-1.,0.,0.));
#7908=DIRECTION('center_axis',(1.,0.,0.));
#7909=DIRECTION('ref_axis',(0.,-1.,0.));
#7910=DIRECTION('center_axis',(-2.96059473233381E-14,1.,0.));
#7911=DIRECTION('ref_axis',(0.,0.,1.));
#7912=DIRECTION('center_axis',(0.,-1.,0.));
#7913=DIRECTION('ref_axis',(-0.707106781186563,0.,0.707106781186532));
#7914=DIRECTION('',(0.,1.,0.));
#7915=DIRECTION('',(0.,-1.,0.));
#7916=DIRECTION('center_axis',(1.,0.,0.));
#7917=DIRECTION('ref_axis',(0.,-0.707106781186547,0.707106781186547));
#7918=DIRECTION('',(-1.,0.,0.));
#7919=DIRECTION('',(1.,0.,0.));
#7920=DIRECTION('center_axis',(0.,0.,-1.));
#7921=DIRECTION('ref_axis',(-0.707106781186558,0.707106781186537,0.));
#7922=DIRECTION('',(0.,0.,1.));
#7923=DIRECTION('',(0.,0.,-1.));
#7924=DIRECTION('center_axis',(0.,0.,-1.));
#7925=DIRECTION('ref_axis',(0.707106781186516,-0.707106781186579,0.));
#7926=DIRECTION('',(0.,0.,1.));
#7927=DIRECTION('',(0.,0.,-1.));
#7928=DIRECTION('center_axis',(0.,0.,1.));
#7929=DIRECTION('ref_axis',(-0.707106781186568,-0.707106781186527,0.));
#7930=DIRECTION('',(0.,0.,1.));
#7931=DIRECTION('',(0.,0.,-1.));
#7932=DIRECTION('center_axis',(0.816496580927728,0.408248290463864,-0.408248290463858));
#7933=DIRECTION('ref_axis',(0.577350269189588,-0.577350269189647,0.577350269189642));
#7934=DIRECTION('center_axis',(0.,0.,-1.));
#7935=DIRECTION('ref_axis',(0.,-1.,0.));
#7936=DIRECTION('center_axis',(0.,1.,0.));
#7937=DIRECTION('ref_axis',(1.,0.,0.));
#7938=DIRECTION('center_axis',(-1.,0.,0.));
#7939=DIRECTION('ref_axis',(0.,0.,1.));
#7940=DIRECTION('center_axis',(0.408248290463857,-0.816496580927726,-0.408248290463869));
#7941=DIRECTION('ref_axis',(-0.57735026918959,-0.577350269189638,0.577350269189649));
#7942=DIRECTION('center_axis',(0.,0.,-1.));
#7943=DIRECTION('ref_axis',(-1.,0.,0.));
#7944=DIRECTION('center_axis',(1.,0.,0.));
#7945=DIRECTION('ref_axis',(0.,-1.,0.));
#7946=DIRECTION('center_axis',(0.,1.,0.));
#7947=DIRECTION('ref_axis',(0.,0.,1.));
#7948=DIRECTION('center_axis',(0.408248290463861,0.408248290463837,-0.81649658092774));
#7949=DIRECTION('ref_axis',(0.577350269189665,0.577350269189606,0.577350269189606));
#7950=DIRECTION('center_axis',(0.,0.,-1.));
#7951=DIRECTION('ref_axis',(1.,0.,0.));
#7952=DIRECTION('center_axis',(-1.,0.,-5.9211894646675E-14));
#7953=DIRECTION('ref_axis',(0.,1.,0.));
#7954=DIRECTION('center_axis',(0.,-1.,0.));
#7955=DIRECTION('ref_axis',(0.,0.,1.));
#7956=DIRECTION('center_axis',(5.9211894646675E-16,1.,0.));
#7957=DIRECTION('ref_axis',(0.707106781186563,0.,0.707106781186532));
#7958=DIRECTION('',(-5.9211894646675E-16,-1.,0.));
#7959=DIRECTION('',(5.9211894646675E-16,1.,0.));
#7960=DIRECTION('center_axis',(-0.408248290463868,-0.816496580927724,0.408248290463862));
#7961=DIRECTION('ref_axis',(-0.577350269189598,0.577350269189634,0.577350269189645));
#7962=DIRECTION('center_axis',(0.,-1.,0.));
#7963=DIRECTION('ref_axis',(-1.,0.,0.));
#7964=DIRECTION('center_axis',(1.,0.,0.));
#7965=DIRECTION('ref_axis',(0.,0.,1.));
#7966=DIRECTION('center_axis',(0.,0.,-1.));
#7967=DIRECTION('ref_axis',(0.,1.,0.));
#7968=DIRECTION('center_axis',(0.,0.,-1.));
#7969=DIRECTION('ref_axis',(-0.707106781186568,0.707106781186527,0.));
#7970=DIRECTION('',(0.,0.,1.));
#7971=DIRECTION('',(0.,0.,-1.));
#7972=DIRECTION('center_axis',(-1.,0.,0.));
#7973=DIRECTION('ref_axis',(0.,0.707106781186553,0.707106781186542));
#7974=DIRECTION('',(1.,0.,0.));
#7975=DIRECTION('',(-1.,0.,0.));
#7976=DIRECTION('center_axis',(0.,-1.,0.));
#7977=DIRECTION('ref_axis',(-0.707106781186563,0.,0.707106781186532));
#7978=DIRECTION('',(0.,1.,0.));
#7979=DIRECTION('',(0.,-1.,0.));
#7980=DIRECTION('center_axis',(0.,0.,1.));
#7981=DIRECTION('ref_axis',(0.707106781186516,0.707106781186579,0.));
#7982=DIRECTION('',(0.,0.,1.));
#7983=DIRECTION('',(0.,0.,-1.));
#7984=DIRECTION('center_axis',(1.,0.,0.));
#7985=DIRECTION('ref_axis',(0.,-0.707106781186553,0.707106781186542));
#7986=DIRECTION('',(-1.,0.,0.));
#7987=DIRECTION('',(1.,0.,0.));
#7988=DIRECTION('center_axis',(0.,0.,1.));
#7989=DIRECTION('ref_axis',(-0.707106781186558,-0.707106781186537,0.));
#7990=DIRECTION('',(0.,0.,1.));
#7991=DIRECTION('',(0.,0.,-1.));
#7992=DIRECTION('center_axis',(1.,0.,0.));
#7993=DIRECTION('ref_axis',(0.,0.,-1.));
#7994=DIRECTION('center_axis',(-1.,0.,0.));
#7995=DIRECTION('ref_axis',(0.,0.,-1.));
#7996=DIRECTION('center_axis',(1.,0.,0.));
#7997=DIRECTION('ref_axis',(0.,0.,-1.));
#7998=DIRECTION('center_axis',(0.,0.,-1.));
#7999=DIRECTION('ref_axis',(0.707106781186516,-0.707106781186579,0.));
#8000=DIRECTION('',(0.,0.,1.));
#8001=DIRECTION('',(0.,0.,-1.));
#8002=DIRECTION('center_axis',(-1.,5.9211894646675E-16,0.));
#8003=DIRECTION('ref_axis',(0.,0.,-1.));
#8004=DIRECTION('center_axis',(-1.,5.9211894646675E-16,0.));
#8005=DIRECTION('ref_axis',(2.62953635073665E-32,4.44089209850053E-17,-1.));
#8006=DIRECTION('center_axis',(1.,-5.9211894646675E-16,0.));
#8007=DIRECTION('ref_axis',(0.,4.44089209850053E-17,-1.));
#8008=DIRECTION('center_axis',(1.,0.,0.));
#8009=DIRECTION('ref_axis',(0.,0.,-1.));
#8010=DIRECTION('center_axis',(1.,0.,0.));
#8011=DIRECTION('ref_axis',(0.,0.,-1.));
#8012=DIRECTION('center_axis',(-1.,0.,0.));
#8013=DIRECTION('ref_axis',(0.,0.,-1.));
#8014=DIRECTION('center_axis',(-1.,5.9211894646675E-16,0.));
#8015=DIRECTION('ref_axis',(0.,0.,-1.));
#8016=DIRECTION('center_axis',(1.,-5.9211894646675E-16,0.));
#8017=DIRECTION('ref_axis',(0.,4.44089209850053E-17,-1.));
#8018=DIRECTION('center_axis',(-1.,5.9211894646675E-16,0.));
#8019=DIRECTION('ref_axis',(2.62953635073665E-32,4.44089209850053E-17,-1.));
#8020=DIRECTION('center_axis',(5.9211894646675E-16,1.,0.));
#8021=DIRECTION('ref_axis',(0.707106781186563,0.,0.707106781186532));
#8022=DIRECTION('',(-5.9211894646675E-16,-1.,0.));
#8023=DIRECTION('',(5.9211894646675E-16,1.,0.));
#8024=DIRECTION('center_axis',(-1.,0.,0.));
#8025=DIRECTION('ref_axis',(0.,0.707106781186547,0.707106781186547));
#8026=DIRECTION('',(1.,0.,0.));
#8027=DIRECTION('',(-1.,0.,0.));
#8028=DIRECTION('center_axis',(0.,-1.,0.));
#8029=DIRECTION('ref_axis',(-0.707106781186563,0.,0.707106781186532));
#8030=DIRECTION('',(0.,1.,0.));
#8031=DIRECTION('',(0.,-1.,0.));
#8032=DIRECTION('center_axis',(1.,0.,0.));
#8033=DIRECTION('ref_axis',(0.,-0.707106781186542,0.707106781186553));
#8034=DIRECTION('',(-1.,0.,0.));
#8035=DIRECTION('',(1.,0.,0.));
#8036=DIRECTION('center_axis',(0.,1.,0.));
#8037=DIRECTION('ref_axis',(-0.707106781186563,0.,0.707106781186532));
#8038=DIRECTION('',(0.,1.,0.));
#8039=DIRECTION('center_axis',(-1.,2.77555756156289E-16,0.));
#8040=DIRECTION('ref_axis',(0.,-0.70710678118654,-0.707106781186555));
#8041=DIRECTION('',(-1.,2.77555756156289E-16,0.));
#8042=DIRECTION('center_axis',(-5.9211894646675E-16,-1.,0.));
#8043=DIRECTION('ref_axis',(0.707106781186521,0.,0.707106781186574));
#8044=DIRECTION('',(-5.9211894646675E-16,-1.,0.));
#8045=DIRECTION('center_axis',(1.,0.,0.));
#8046=DIRECTION('ref_axis',(0.,0.70710678118654,-0.707106781186555));
#8047=DIRECTION('',(1.,0.,0.));
#8048=DIRECTION('center_axis',(0.,-1.,0.));
#8049=DIRECTION('ref_axis',(-0.707106781186563,0.,0.707106781186532));
#8050=DIRECTION('',(0.,1.,0.));
#8051=DIRECTION('center_axis',(0.,0.,-1.));
#8052=DIRECTION('ref_axis',(-0.707106781186568,0.707106781186527,0.));
#8053=DIRECTION('',(0.,0.,1.));
#8054=DIRECTION('',(0.,0.,-1.));
#8055=DIRECTION('center_axis',(5.9211894646675E-16,1.,0.));
#8056=DIRECTION('ref_axis',(0.707106781186563,0.,0.707106781186532));
#8057=DIRECTION('',(-5.9211894646675E-16,-1.,0.));
#8058=DIRECTION('center_axis',(0.,0.,-1.));
#8059=DIRECTION('ref_axis',(0.707106781186516,0.707106781186579,0.));
#8060=DIRECTION('',(0.,0.,1.));
#8061=DIRECTION('',(0.,0.,-1.));
#8062=DIRECTION('center_axis',(1.,0.,0.));
#8063=DIRECTION('ref_axis',(0.,-0.707106781186553,0.707106781186542));
#8064=DIRECTION('',(-1.,0.,0.));
#8065=DIRECTION('center_axis',(-1.,0.,0.));
#8066=DIRECTION('ref_axis',(0.,-0.707106781186547,-0.707106781186547));
#8067=DIRECTION('',(1.,0.,0.));
#8068=DIRECTION('',(-1.,0.,0.));
#8069=DIRECTION('center_axis',(0.,-1.,0.));
#8070=DIRECTION('ref_axis',(0.,0.,1.));
#8071=DIRECTION('',(-1.,0.,0.));
#8072=DIRECTION('center_axis',(-1.,0.,0.));
#8073=DIRECTION('ref_axis',(0.,6.12323399573677E-17,-1.));
#8074=DIRECTION('',(-1.,0.,0.));
#8075=DIRECTION('center_axis',(1.,0.,0.));
#8076=DIRECTION('ref_axis',(0.,-6.12323399573677E-17,-1.));
#8077=DIRECTION('',(-1.,0.,0.));
#8078=DIRECTION('',(-1.,0.,0.));
#8079=DIRECTION('center_axis',(0.,-1.,0.));
#8080=DIRECTION('ref_axis',(0.,0.,1.));
#8081=DIRECTION('center_axis',(0.,0.,1.));
#8082=DIRECTION('ref_axis',(1.,0.,0.));
#8083=DIRECTION('center_axis',(0.,1.,0.));
#8084=DIRECTION('ref_axis',(-1.,0.,0.));
#8085=DIRECTION('center_axis',(0.,1.,0.));
#8086=DIRECTION('ref_axis',(-1.,0.,0.));
#8087=DIRECTION('center_axis',(0.,1.,0.));
#8088=DIRECTION('ref_axis',(-1.,0.,0.));
#8089=DIRECTION('center_axis',(0.,0.,-1.));
#8090=DIRECTION('ref_axis',(-1.,0.,0.));
#8091=DIRECTION('center_axis',(-2.77555756156289E-16,-1.,0.));
#8092=DIRECTION('ref_axis',(1.,-2.77555756156289E-16,0.));
#8093=DIRECTION('center_axis',(0.,0.,-1.));
#8094=DIRECTION('ref_axis',(-1.,0.,0.));
#8095=DIRECTION('center_axis',(-1.,5.9211894646675E-16,0.));
#8096=DIRECTION('ref_axis',(-5.9211894646675E-16,-1.,0.));
#8097=DIRECTION('center_axis',(0.,0.,-1.));
#8098=DIRECTION('ref_axis',(-1.,0.,0.));
#8099=DIRECTION('center_axis',(1.,0.,0.));
#8100=DIRECTION('ref_axis',(0.,1.,0.));
#8101=DIRECTION('center_axis',(0.,1.,0.));
#8102=DIRECTION('ref_axis',(0.,0.,-1.));
#8103=DIRECTION('center_axis',(0.,1.,0.));
#8104=DIRECTION('ref_axis',(0.,0.,-1.));
#9495=CARTESIAN_POINT('',(0.,0.,0.));
#9496=CARTESIAN_POINT('Origin',(133.037195913696,35.,-10.3));
#9497=CARTESIAN_POINT('',(135.037195913696,35.,-10.3));
#9498=CARTESIAN_POINT('Origin',(133.037195913696,35.,-10.3));
#9499=CARTESIAN_POINT('',(135.337195913696,35.,-10.));
#9500=CARTESIAN_POINT('Origin',(135.337195913696,35.,-10.3));
#9501=CARTESIAN_POINT('Origin',(133.037195913696,35.,-10.));
#9502=CARTESIAN_POINT('Origin',(137.,35.,-10.));
#9503=CARTESIAN_POINT('',(144.7,39.7,-10.));
#9504=CARTESIAN_POINT('',(129.3,39.7,-10.));
#9505=CARTESIAN_POINT('',(141.,39.7,-10.));
#9506=CARTESIAN_POINT('',(129.3,30.3,-10.));
#9507=CARTESIAN_POINT('',(129.3,2.5,-10.));
#9508=CARTESIAN_POINT('',(144.7,30.3,-10.));
#9509=CARTESIAN_POINT('',(133.,30.3,-10.));
#9510=CARTESIAN_POINT('',(144.7,32.5,-10.));
#9511=CARTESIAN_POINT('',(143.262804086304,35.,-10.));
#9512=CARTESIAN_POINT('Origin',(140.962804086304,35.,-10.));
#9513=CARTESIAN_POINT('Origin',(133.037195913696,35.,-16.));
#9514=CARTESIAN_POINT('',(135.037195913696,35.,-16.));
#9515=CARTESIAN_POINT('',(135.037195913696,35.,-16.));
#9516=CARTESIAN_POINT('Origin',(133.037195913696,35.,-16.));
#9517=CARTESIAN_POINT('Origin',(140.962804086304,35.,-10.3));
#9518=CARTESIAN_POINT('',(142.962804086304,35.,-10.3));
#9519=CARTESIAN_POINT('Origin',(140.962804086304,35.,-10.3));
#9520=CARTESIAN_POINT('Origin',(143.262804086304,35.,-10.3));
#9521=CARTESIAN_POINT('Origin',(140.962804086304,35.,-16.));
#9522=CARTESIAN_POINT('',(142.962804086304,35.,-16.));
#9523=CARTESIAN_POINT('',(142.962804086304,35.,-16.));
#9524=CARTESIAN_POINT('Origin',(140.962804086304,35.,-16.));
#9525=CARTESIAN_POINT('Origin',(133.037195913696,-35.,-10.3));
#9526=CARTESIAN_POINT('',(130.737195913696,-35.,-10.));
#9527=CARTESIAN_POINT('Origin',(133.037195913696,-35.,-10.));
#9528=CARTESIAN_POINT('',(131.037195913696,-35.,-10.3));
#9529=CARTESIAN_POINT('Origin',(130.737195913696,-35.,-10.3));
#9530=CARTESIAN_POINT('',(135.037195913696,-35.,-10.3));
#9531=CARTESIAN_POINT('Origin',(133.037195913696,-35.,-10.3));
#9532=CARTESIAN_POINT('Origin',(133.037195913696,-35.,-10.3));
#9533=CARTESIAN_POINT('Origin',(137.,-35.,-10.));
#9534=CARTESIAN_POINT('',(144.7,-30.3,-10.));
#9535=CARTESIAN_POINT('',(129.3,-30.3,-10.));
#9536=CARTESIAN_POINT('',(141.,-30.3,-10.));
#9537=CARTESIAN_POINT('',(129.3,-39.7,-10.));
#9538=CARTESIAN_POINT('',(129.3,-32.5,-10.));
#9539=CARTESIAN_POINT('',(144.7,-39.7,-10.));
#9540=CARTESIAN_POINT('',(141.,-39.7,-10.));
#9541=CARTESIAN_POINT('',(144.7,-2.5,-10.));
#9542=CARTESIAN_POINT('',(138.662804086304,-35.,-10.));
#9543=CARTESIAN_POINT('Origin',(140.962804086304,-35.,-10.));
#9544=CARTESIAN_POINT('Origin',(133.037195913696,-35.,-16.));
#9545=CARTESIAN_POINT('',(135.037195913696,-35.,-16.));
#9546=CARTESIAN_POINT('',(135.037195913696,-35.,-16.));
#9547=CARTESIAN_POINT('Origin',(133.037195913696,-35.,-16.));
#9548=CARTESIAN_POINT('Origin',(140.962804086304,-35.,-10.3));
#9549=CARTESIAN_POINT('',(138.962804086304,-35.,-10.3));
#9550=CARTESIAN_POINT('Origin',(138.662804086304,-35.,-10.3));
#9551=CARTESIAN_POINT('',(142.962804086304,-35.,-10.3));
#9552=CARTESIAN_POINT('Origin',(140.962804086304,-35.,-10.3));
#9553=CARTESIAN_POINT('Origin',(140.962804086304,-35.,-10.3));
#9554=CARTESIAN_POINT('Origin',(140.962804086304,-35.,-16.));
#9555=CARTESIAN_POINT('',(142.962804086304,-35.,-16.));
#9556=CARTESIAN_POINT('',(142.962804086304,-35.,-16.));
#9557=CARTESIAN_POINT('Origin',(140.962804086304,-35.,-16.));
#9558=CARTESIAN_POINT('Origin',(144.7,-39.7,-15.7));
#9559=CARTESIAN_POINT('',(145.,-39.7,-15.7));
#9560=CARTESIAN_POINT('',(144.7,-40.,-15.7));
#9561=CARTESIAN_POINT('Origin',(144.7,-39.7,-15.7));
#9562=CARTESIAN_POINT('',(144.7,-39.7,-16.));
#9563=CARTESIAN_POINT('Origin',(144.7,-39.7,-15.7));
#9564=CARTESIAN_POINT('Origin',(144.7,-39.7,-15.7));
#9565=CARTESIAN_POINT('Origin',(129.3,-39.7,-15.7));
#9566=CARTESIAN_POINT('',(129.3,-39.7,-16.));
#9567=CARTESIAN_POINT('',(129.3,-40.,-15.7));
#9568=CARTESIAN_POINT('Origin',(129.3,-39.7,-15.7));
#9569=CARTESIAN_POINT('',(129.,-39.7,-15.7));
#9570=CARTESIAN_POINT('Origin',(129.3,-39.7,-15.7));
#9571=CARTESIAN_POINT('Origin',(129.3,-39.7,-15.7));
#9572=CARTESIAN_POINT('Origin',(144.7,39.7,-15.7));
#9573=CARTESIAN_POINT('',(144.7,39.7,-16.));
#9574=CARTESIAN_POINT('',(144.7,40.,-15.7));
#9575=CARTESIAN_POINT('Origin',(144.7,39.7,-15.7));
#9576=CARTESIAN_POINT('',(145.,39.7,-15.7));
#9577=CARTESIAN_POINT('Origin',(144.7,39.7,-15.7));
#9578=CARTESIAN_POINT('Origin',(144.7,39.7,-15.7));
#9579=CARTESIAN_POINT('Origin',(144.7,15.,-15.7));
#9580=CARTESIAN_POINT('',(145.,15.,-15.7));
#9581=CARTESIAN_POINT('',(144.7,15.,-16.));
#9582=CARTESIAN_POINT('Origin',(144.7,-39.7,-10.3));
#9583=CARTESIAN_POINT('',(145.,-39.7,-10.3));
#9584=CARTESIAN_POINT('Origin',(144.7,-39.7,-10.3));
#9585=CARTESIAN_POINT('',(144.7,-40.,-10.3));
#9586=CARTESIAN_POINT('Origin',(144.7,-39.7,-10.3));
#9587=CARTESIAN_POINT('Origin',(144.7,-39.7,-10.3));
#9588=CARTESIAN_POINT('Origin',(144.7,-39.7,-8.));
#9589=CARTESIAN_POINT('',(144.7,-40.,-8.));
#9590=CARTESIAN_POINT('',(145.,-39.7,-8.));
#9591=CARTESIAN_POINT('Origin',(129.3,39.7,-15.7));
#9592=CARTESIAN_POINT('',(129.,39.7,-15.7));
#9593=CARTESIAN_POINT('',(129.3,40.,-15.7));
#9594=CARTESIAN_POINT('Origin',(129.3,39.7,-15.7));
#9595=CARTESIAN_POINT('',(129.3,39.7,-16.));
#9596=CARTESIAN_POINT('Origin',(129.3,39.7,-15.7));
#9597=CARTESIAN_POINT('Origin',(129.3,39.7,-15.7));
#9598=CARTESIAN_POINT('Origin',(129.3,-15.,-15.7));
#9599=CARTESIAN_POINT('',(129.3,-15.,-16.));
#9600=CARTESIAN_POINT('',(129.,-15.,-15.7));
#9601=CARTESIAN_POINT('Origin',(141.,39.7,-15.7));
#9602=CARTESIAN_POINT('',(141.,39.7,-16.));
#9603=CARTESIAN_POINT('',(141.,40.,-15.7));
#9604=CARTESIAN_POINT('Origin',(129.3,-39.7,-10.3));
#9605=CARTESIAN_POINT('',(129.3,-40.,-10.3));
#9606=CARTESIAN_POINT('Origin',(129.3,-39.7,-10.3));
#9607=CARTESIAN_POINT('',(129.,-39.7,-10.3));
#9608=CARTESIAN_POINT('Origin',(129.3,-39.7,-10.3));
#9609=CARTESIAN_POINT('Origin',(129.3,-39.7,-10.3));
#9610=CARTESIAN_POINT('Origin',(129.3,-39.7,-8.));
#9611=CARTESIAN_POINT('',(129.,-39.7,-8.));
#9612=CARTESIAN_POINT('',(129.3,-40.,-8.));
#9613=CARTESIAN_POINT('Origin',(144.7,39.7,-10.3));
#9614=CARTESIAN_POINT('',(145.,39.7,-10.3));
#9615=CARTESIAN_POINT('',(144.7,40.,-10.3));
#9616=CARTESIAN_POINT('Origin',(144.7,39.7,-10.3));
#9617=CARTESIAN_POINT('Origin',(144.7,39.7,-10.3));
#9618=CARTESIAN_POINT('Origin',(144.7,39.7,-10.3));
#9619=CARTESIAN_POINT('Origin',(144.7,-30.3,-9.7));
#9620=CARTESIAN_POINT('',(144.7,-30.,-9.7));
#9621=CARTESIAN_POINT('Origin',(144.7,-30.3,-9.7));
#9622=CARTESIAN_POINT('',(145.,-30.3,-10.3));
#9623=CARTESIAN_POINT('Origin',(144.7,-30.3,-10.3));
#9624=CARTESIAN_POINT('',(145.,-29.7,-9.7));
#9625=CARTESIAN_POINT('Origin',(145.,-30.3,-9.7));
#9626=CARTESIAN_POINT('Origin',(144.7,-29.7,-9.7));
#9627=CARTESIAN_POINT('Origin',(129.3,39.7,-10.3));
#9628=CARTESIAN_POINT('',(129.3,40.,-10.3));
#9629=CARTESIAN_POINT('',(129.,39.7,-10.3));
#9630=CARTESIAN_POINT('Origin',(129.3,39.7,-10.3));
#9631=CARTESIAN_POINT('Origin',(129.3,39.7,-10.3));
#9632=CARTESIAN_POINT('Origin',(129.3,39.7,-10.3));
#9633=CARTESIAN_POINT('Origin',(141.,39.7,-10.3));
#9634=CARTESIAN_POINT('',(141.,40.,-10.3));
#9635=CARTESIAN_POINT('Origin',(129.3,-30.3,-9.7));
#9636=CARTESIAN_POINT('',(129.,-30.3,-10.3));
#9637=CARTESIAN_POINT('',(129.,-29.7,-9.7));
#9638=CARTESIAN_POINT('Origin',(129.,-30.3,-9.7));
#9639=CARTESIAN_POINT('Origin',(129.3,-30.3,-10.3));
#9640=CARTESIAN_POINT('',(129.3,-30.,-9.7));
#9641=CARTESIAN_POINT('Origin',(129.3,-30.3,-9.7));
#9642=CARTESIAN_POINT('Origin',(129.3,-29.7,-9.7));
#9643=CARTESIAN_POINT('Origin',(144.7,30.3,-9.7));
#9644=CARTESIAN_POINT('',(145.,30.3,-10.3));
#9645=CARTESIAN_POINT('',(145.,29.7,-9.7));
#9646=CARTESIAN_POINT('Origin',(145.,30.3,-9.7));
#9647=CARTESIAN_POINT('Origin',(144.7,30.3,-10.3));
#9648=CARTESIAN_POINT('',(144.7,30.,-9.7));
#9649=CARTESIAN_POINT('Origin',(144.7,30.3,-9.7));
#9650=CARTESIAN_POINT('Origin',(144.7,29.7,-9.7));
#9651=CARTESIAN_POINT('Origin',(144.7,-29.7,15.7));
#9652=CARTESIAN_POINT('',(145.,-29.7,15.7));
#9653=CARTESIAN_POINT('',(144.7,-29.7,16.));
#9654=CARTESIAN_POINT('Origin',(144.7,-29.7,15.7));
#9655=CARTESIAN_POINT('',(144.7,-30.,15.7));
#9656=CARTESIAN_POINT('Origin',(144.7,-29.7,15.7));
#9657=CARTESIAN_POINT('Origin',(144.7,-29.7,15.7));
#9658=CARTESIAN_POINT('Origin',(144.7,-29.7,0.));
#9659=CARTESIAN_POINT('',(145.,-29.7,0.));
#9660=CARTESIAN_POINT('',(144.7,-30.,0.));
#9661=CARTESIAN_POINT('Origin',(129.3,30.3,-9.7));
#9662=CARTESIAN_POINT('',(129.3,30.,-9.7));
#9663=CARTESIAN_POINT('Origin',(129.3,30.3,-9.7));
#9664=CARTESIAN_POINT('',(129.,30.3,-10.3));
#9665=CARTESIAN_POINT('Origin',(129.3,30.3,-10.3));
#9666=CARTESIAN_POINT('',(129.,29.7,-9.7));
#9667=CARTESIAN_POINT('Origin',(129.,30.3,-9.7));
#9668=CARTESIAN_POINT('Origin',(129.3,29.7,-9.7));
#9669=CARTESIAN_POINT('Origin',(129.3,-29.7,15.7));
#9670=CARTESIAN_POINT('',(129.3,-30.,15.7));
#9671=CARTESIAN_POINT('',(129.3,-29.7,16.));
#9672=CARTESIAN_POINT('Origin',(129.3,-29.7,15.7));
#9673=CARTESIAN_POINT('',(129.,-29.7,15.7));
#9674=CARTESIAN_POINT('Origin',(129.3,-29.7,15.7));
#9675=CARTESIAN_POINT('Origin',(129.3,-29.7,15.7));
#9676=CARTESIAN_POINT('Origin',(129.3,-29.7,0.));
#9677=CARTESIAN_POINT('',(129.,-29.7,0.));
#9678=CARTESIAN_POINT('',(129.3,-30.,0.));
#9679=CARTESIAN_POINT('Origin',(144.7,29.7,15.7));
#9680=CARTESIAN_POINT('',(144.7,30.,15.7));
#9681=CARTESIAN_POINT('',(144.7,29.7,16.));
#9682=CARTESIAN_POINT('Origin',(144.7,29.7,15.7));
#9683=CARTESIAN_POINT('',(145.,29.7,15.7));
#9684=CARTESIAN_POINT('Origin',(144.7,29.7,15.7));
#9685=CARTESIAN_POINT('Origin',(144.7,29.7,15.7));
#9686=CARTESIAN_POINT('Origin',(144.7,29.7,0.));
#9687=CARTESIAN_POINT('',(145.,29.7,0.));
#9688=CARTESIAN_POINT('',(144.7,30.,0.));
#9689=CARTESIAN_POINT('Origin',(144.7,-22.7999999999999,15.7));
#9690=CARTESIAN_POINT('',(145.,-22.7999999999999,15.7));
#9691=CARTESIAN_POINT('',(144.7,-22.4999999999999,15.7));
#9692=CARTESIAN_POINT('Origin',(144.7,-22.7999999999999,15.7));
#9693=CARTESIAN_POINT('',(144.7,-22.7999999999999,16.));
#9694=CARTESIAN_POINT('Origin',(144.7,-22.7999999999999,15.7));
#9695=CARTESIAN_POINT('Origin',(144.7,-22.7999999999999,15.7));
#9696=CARTESIAN_POINT('Origin',(144.7,15.,15.7));
#9697=CARTESIAN_POINT('',(145.,15.,15.7));
#9698=CARTESIAN_POINT('',(144.7,15.,16.));
#9699=CARTESIAN_POINT('Origin',(129.3,29.7,15.7));
#9700=CARTESIAN_POINT('',(129.,29.7,15.7));
#9701=CARTESIAN_POINT('',(129.3,29.7,16.));
#9702=CARTESIAN_POINT('Origin',(129.3,29.7,15.7));
#9703=CARTESIAN_POINT('',(129.3,30.,15.7));
#9704=CARTESIAN_POINT('Origin',(129.3,29.7,15.7));
#9705=CARTESIAN_POINT('Origin',(129.3,29.7,15.7));
#9706=CARTESIAN_POINT('Origin',(129.3,29.7,0.));
#9707=CARTESIAN_POINT('',(129.3,30.,0.));
#9708=CARTESIAN_POINT('',(129.,29.7,0.));
#9709=CARTESIAN_POINT('Origin',(133.,29.7,15.7));
#9710=CARTESIAN_POINT('',(133.,30.,15.7));
#9711=CARTESIAN_POINT('',(133.,29.7,16.));
#9712=CARTESIAN_POINT('Origin',(129.3,-22.7999999999999,15.7));
#9713=CARTESIAN_POINT('',(129.,-22.7999999999999,15.7));
#9714=CARTESIAN_POINT('',(129.3,-22.7999999999999,16.));
#9715=CARTESIAN_POINT('Origin',(129.3,-22.7999999999999,15.7));
#9716=CARTESIAN_POINT('',(129.3,-22.4999999999999,15.7));
#9717=CARTESIAN_POINT('Origin',(129.3,-22.7999999999999,15.7));
#9718=CARTESIAN_POINT('Origin',(129.3,-22.7999999999999,15.7));
#9719=CARTESIAN_POINT('Origin',(144.7,22.7999999999999,15.7));
#9720=CARTESIAN_POINT('',(144.7,22.4999999999999,15.7));
#9721=CARTESIAN_POINT('',(145.,22.7999999999999,15.7));
#9722=CARTESIAN_POINT('Origin',(144.7,22.7999999999999,15.7));
#9723=CARTESIAN_POINT('',(144.7,22.7999999999999,16.));
#9724=CARTESIAN_POINT('Origin',(144.7,22.7999999999999,15.7));
#9725=CARTESIAN_POINT('Origin',(144.7,22.7999999999999,15.7));
#9726=CARTESIAN_POINT('Origin',(144.7,-22.7999999999999,8.));
#9727=CARTESIAN_POINT('',(145.,-22.7999999999999,2.29525996204705));
#9728=CARTESIAN_POINT('',(145.,-22.7999999999999,8.));
#9729=CARTESIAN_POINT('',(144.7,-22.4999999999999,2.03896089378841));
#9730=CARTESIAN_POINT('Ctrl Pts',(144.7,-22.4999999999999,2.03896089378841));
#9731=CARTESIAN_POINT('Ctrl Pts',(144.729707021216,-22.4999999999999,2.03896089378841));
#9732=CARTESIAN_POINT('Ctrl Pts',(144.758777673282,-22.5044062942651,2.04285168076791));
#9733=CARTESIAN_POINT('Ctrl Pts',(144.817440852233,-22.5220432289933,2.05836227087722));
#9734=CARTESIAN_POINT('Ctrl Pts',(144.845615509175,-22.5359942380498,2.07060652861162));
#9735=CARTESIAN_POINT('Ctrl Pts',(144.902101216584,-22.5749600084548,2.10457296342855));
#9736=CARTESIAN_POINT('Ctrl Pts',(144.927927434013,-22.6017796731997,2.12780612534896));
#9737=CARTESIAN_POINT('Ctrl Pts',(144.964853191741,-22.6558870245156,2.17419410934337));
#9738=CARTESIAN_POINT('Ctrl Pts',(144.977648024164,-22.6827478353212,2.19704892778962));
#9739=CARTESIAN_POINT('Ctrl Pts',(144.995183002528,-22.7387435986925,2.24427435404391));
#9740=CARTESIAN_POINT('Ctrl Pts',(144.999750204092,-22.768135790235,2.26885093228759));
#9741=CARTESIAN_POINT('Ctrl Pts',(144.999996676585,-22.7983695157586,2.29390907943587));
#9742=CARTESIAN_POINT('Ctrl Pts',(145.,-22.7991847191594,2.29458456964534));
#9743=CARTESIAN_POINT('Ctrl Pts',(145.,-22.7999999999999,2.29525996204705));
#9744=CARTESIAN_POINT('',(144.7,-22.4999999999999,8.));
#9745=CARTESIAN_POINT('Origin',(129.3,22.7999999999999,15.7));
#9746=CARTESIAN_POINT('',(129.,22.7999999999999,15.7));
#9747=CARTESIAN_POINT('',(129.3,22.4999999999999,15.7));
#9748=CARTESIAN_POINT('Origin',(129.3,22.7999999999999,15.7));
#9749=CARTESIAN_POINT('',(129.3,22.7999999999999,16.));
#9750=CARTESIAN_POINT('Origin',(129.3,22.7999999999999,15.7));
#9751=CARTESIAN_POINT('Origin',(129.3,22.7999999999999,15.7));
#9752=CARTESIAN_POINT('Origin',(129.3,-15.,15.7));
#9753=CARTESIAN_POINT('',(129.,-15.,15.7));
#9754=CARTESIAN_POINT('',(129.3,-15.,16.));
#9755=CARTESIAN_POINT('Origin',(141.,22.7999999999999,15.7));
#9756=CARTESIAN_POINT('',(141.,22.4999999999999,15.7));
#9757=CARTESIAN_POINT('',(141.,22.7999999999999,16.));
#9758=CARTESIAN_POINT('Origin',(129.3,-22.7999999999999,8.));
#9759=CARTESIAN_POINT('',(129.3,-22.4999999999999,2.03896089378841));
#9760=CARTESIAN_POINT('',(129.3,-22.4999999999999,8.));
#9761=CARTESIAN_POINT('',(129.,-22.7999999999999,2.29525996204705));
#9762=CARTESIAN_POINT('Ctrl Pts',(129.,-22.7999999999999,2.29525996204705));
#9763=CARTESIAN_POINT('Ctrl Pts',(129.,-22.7991847191433,2.29458456963201));
#9764=CARTESIAN_POINT('Ctrl Pts',(129.000003323414,-22.798369515774,2.29390907945453));
#9765=CARTESIAN_POINT('Ctrl Pts',(129.000249795909,-22.7681357900482,2.26885093208373));
#9766=CARTESIAN_POINT('Ctrl Pts',(129.004816997483,-22.7387435986578,2.24427435401478));
#9767=CARTESIAN_POINT('Ctrl Pts',(129.022351975836,-22.6827478353226,2.19704892779083));
#9768=CARTESIAN_POINT('Ctrl Pts',(129.035146808259,-22.6558870245162,2.17419410934394));
#9769=CARTESIAN_POINT('Ctrl Pts',(129.072072565987,-22.6017796731997,2.12780612534895));
#9770=CARTESIAN_POINT('Ctrl Pts',(129.097898783416,-22.5749600084547,2.10457296342854));
#9771=CARTESIAN_POINT('Ctrl Pts',(129.154384490824,-22.5359942380497,2.07060652861162));
#9772=CARTESIAN_POINT('Ctrl Pts',(129.182559147767,-22.5220432289933,2.05836227087722));
#9773=CARTESIAN_POINT('Ctrl Pts',(129.241222326718,-22.5044062942651,2.04285168076791));
#9774=CARTESIAN_POINT('Ctrl Pts',(129.270292978784,-22.4999999999999,2.03896089378841));
#9775=CARTESIAN_POINT('Ctrl Pts',(129.3,-22.4999999999999,2.03896089378841));
#9776=CARTESIAN_POINT('',(129.,-22.7999999999999,8.));
#9777=CARTESIAN_POINT('Origin',(144.7,22.7999999999999,8.));
#9778=CARTESIAN_POINT('',(144.7,22.4999999999999,2.03896089378841));
#9779=CARTESIAN_POINT('',(144.7,22.4999999999999,8.));
#9780=CARTESIAN_POINT('',(145.,22.7999999999999,2.29525996204705));
#9781=CARTESIAN_POINT('Ctrl Pts',(145.,22.7999999999999,2.29525996204705));
#9782=CARTESIAN_POINT('Ctrl Pts',(145.,22.7991847191433,2.29458456963199));
#9783=CARTESIAN_POINT('Ctrl Pts',(144.999996676586,22.798369515774,2.29390907945454));
#9784=CARTESIAN_POINT('Ctrl Pts',(144.99975020409,22.768135790048,2.26885093208354));
#9785=CARTESIAN_POINT('Ctrl Pts',(144.995183002517,22.7387435986577,2.24427435401474));
#9786=CARTESIAN_POINT('Ctrl Pts',(144.977648024164,22.6827478353226,2.19704892779082));
#9787=CARTESIAN_POINT('Ctrl Pts',(144.964853191741,22.6558870245162,2.17419410934393));
#9788=CARTESIAN_POINT('Ctrl Pts',(144.927927434013,22.6017796731997,2.12780612534896));
#9789=CARTESIAN_POINT('Ctrl Pts',(144.902101216584,22.5749600084548,2.10457296342855));
#9790=CARTESIAN_POINT('Ctrl Pts',(144.845615509175,22.5359942380498,2.07060652861164));
#9791=CARTESIAN_POINT('Ctrl Pts',(144.817440852233,22.5220432289933,2.05836227087723));
#9792=CARTESIAN_POINT('Ctrl Pts',(144.758777673282,22.5044062942651,2.04285168076791));
#9793=CARTESIAN_POINT('Ctrl Pts',(144.729707021216,22.4999999999999,2.03896089378841));
#9794=CARTESIAN_POINT('Ctrl Pts',(144.7,22.4999999999999,2.03896089378841));
#9795=CARTESIAN_POINT('',(145.,22.7999999999999,8.));
#9796=CARTESIAN_POINT('Origin',(129.3,22.7999999999999,8.));
#9797=CARTESIAN_POINT('',(129.,22.7999999999999,2.29525996204705));
#9798=CARTESIAN_POINT('',(129.,22.7999999999999,8.));
#9799=CARTESIAN_POINT('',(129.3,22.4999999999999,2.03896089378841));
#9800=CARTESIAN_POINT('Ctrl Pts',(129.3,22.4999999999999,2.03896089378841));
#9801=CARTESIAN_POINT('Ctrl Pts',(129.270292978784,22.4999999999999,2.03896089378841));
#9802=CARTESIAN_POINT('Ctrl Pts',(129.241222326718,22.5044062942651,2.04285168076791));
#9803=CARTESIAN_POINT('Ctrl Pts',(129.182559147767,22.5220432289932,2.05836227087722));
#9804=CARTESIAN_POINT('Ctrl Pts',(129.154384490824,22.5359942380497,2.07060652861162));
#9805=CARTESIAN_POINT('Ctrl Pts',(129.097898783416,22.5749600084547,2.10457296342855));
#9806=CARTESIAN_POINT('Ctrl Pts',(129.072072565987,22.6017796731997,2.12780612534895));
#9807=CARTESIAN_POINT('Ctrl Pts',(129.035146808259,22.6558870245162,2.17419410934394));
#9808=CARTESIAN_POINT('Ctrl Pts',(129.022351975836,22.6827478353226,2.19704892779082));
#9809=CARTESIAN_POINT('Ctrl Pts',(129.004816997483,22.7387435986577,2.24427435401479));
#9810=CARTESIAN_POINT('Ctrl Pts',(129.000249795909,22.7681357900482,2.26885093208374));
#9811=CARTESIAN_POINT('Ctrl Pts',(129.000003323414,22.798369515774,2.29390907945453));
#9812=CARTESIAN_POINT('Ctrl Pts',(129.,22.7991847191433,2.29458456963201));
#9813=CARTESIAN_POINT('Ctrl Pts',(129.,22.7999999999999,2.29525996204705));
#9814=CARTESIAN_POINT('',(129.3,22.4999999999999,8.));
#9815=CARTESIAN_POINT('Origin',(144.7,-21.1999999999999,15.7));
#9816=CARTESIAN_POINT('',(144.7,-21.4999999999999,15.7));
#9817=CARTESIAN_POINT('',(145.,-21.1999999999999,15.7));
#9818=CARTESIAN_POINT('Origin',(144.7,-21.1999999999999,15.7));
#9819=CARTESIAN_POINT('',(144.7,-21.1999999999999,16.));
#9820=CARTESIAN_POINT('Origin',(144.7,-21.1999999999999,15.7));
#9821=CARTESIAN_POINT('Origin',(144.7,-21.1999999999999,15.7));
#9822=CARTESIAN_POINT('Origin',(129.3,-21.1999999999999,15.7));
#9823=CARTESIAN_POINT('',(129.,-21.1999999999999,15.7));
#9824=CARTESIAN_POINT('',(129.3,-21.4999999999999,15.7));
#9825=CARTESIAN_POINT('Origin',(129.3,-21.1999999999999,15.7));
#9826=CARTESIAN_POINT('',(129.3,-21.1999999999999,16.));
#9827=CARTESIAN_POINT('Origin',(129.3,-21.1999999999999,15.7));
#9828=CARTESIAN_POINT('Origin',(129.3,-21.1999999999999,15.7));
#9829=CARTESIAN_POINT('Origin',(144.7,21.1999999999999,15.7));
#9830=CARTESIAN_POINT('',(145.,21.1999999999999,15.7));
#9831=CARTESIAN_POINT('',(144.7,21.4999999999999,15.7));
#9832=CARTESIAN_POINT('Origin',(144.7,21.1999999999999,15.7));
#9833=CARTESIAN_POINT('',(144.7,21.1999999999999,16.));
#9834=CARTESIAN_POINT('Origin',(144.7,21.1999999999999,15.7));
#9835=CARTESIAN_POINT('Origin',(144.7,21.1999999999999,15.7));
#9836=CARTESIAN_POINT('Origin',(144.7,15.,15.7));
#9837=CARTESIAN_POINT('',(145.,15.,15.7));
#9838=CARTESIAN_POINT('',(144.7,15.,16.));
#9839=CARTESIAN_POINT('Origin',(129.3,21.1999999999999,15.7));
#9840=CARTESIAN_POINT('',(129.,21.1999999999999,15.7));
#9841=CARTESIAN_POINT('',(129.3,21.1999999999999,16.));
#9842=CARTESIAN_POINT('Origin',(129.3,21.1999999999999,15.7));
#9843=CARTESIAN_POINT('',(129.3,21.4999999999999,15.7));
#9844=CARTESIAN_POINT('Origin',(129.3,21.1999999999999,15.7));
#9845=CARTESIAN_POINT('Origin',(129.3,21.1999999999999,15.7));
#9846=CARTESIAN_POINT('Origin',(129.3,21.1999999999999,1.01948044689421));
#9847=CARTESIAN_POINT('',(129.3,21.4999999999999,2.03896089378841));
#9848=CARTESIAN_POINT('',(129.3,21.4999999999999,1.01948044689421));
#9849=CARTESIAN_POINT('',(129.,21.1999999999999,2.29525996204705));
#9850=CARTESIAN_POINT('Ctrl Pts',(129.,21.1999999999999,2.29525996204705));
#9851=CARTESIAN_POINT('Ctrl Pts',(129.,21.2008152808565,2.29458456963201));
#9852=CARTESIAN_POINT('Ctrl Pts',(129.000003323414,21.2016304842259,2.29390907945453));
#9853=CARTESIAN_POINT('Ctrl Pts',(129.000249795909,21.2318642099517,2.26885093208371));
#9854=CARTESIAN_POINT('Ctrl Pts',(129.004816997483,21.2612564013421,2.24427435401476));
#9855=CARTESIAN_POINT('Ctrl Pts',(129.022351975836,21.3172521646773,2.19704892779083));
#9856=CARTESIAN_POINT('Ctrl Pts',(129.035146808259,21.3441129754836,2.17419410934394));
#9857=CARTESIAN_POINT('Ctrl Pts',(129.072072565987,21.3982203268002,2.12780612534896));
#9858=CARTESIAN_POINT('Ctrl Pts',(129.097898783416,21.4250399915451,2.10457296342855));
#9859=CARTESIAN_POINT('Ctrl Pts',(129.154384490824,21.4640057619501,2.07060652861162));
#9860=CARTESIAN_POINT('Ctrl Pts',(129.182559147767,21.4779567710066,2.05836227087723));
#9861=CARTESIAN_POINT('Ctrl Pts',(129.241222326718,21.4955937057348,2.04285168076791));
#9862=CARTESIAN_POINT('Ctrl Pts',(129.270292978784,21.4999999999999,2.03896089378841));
#9863=CARTESIAN_POINT('Ctrl Pts',(129.3,21.4999999999999,2.03896089378841));
#9864=CARTESIAN_POINT('',(129.,21.1999999999999,1.01948044689421));
#9865=CARTESIAN_POINT('Origin',(141.,21.1999999999999,15.7));
#9866=CARTESIAN_POINT('',(141.,21.4999999999999,15.7));
#9867=CARTESIAN_POINT('',(141.,21.1999999999999,16.));
#9868=CARTESIAN_POINT('Origin',(129.3,-15.,15.7));
#9869=CARTESIAN_POINT('',(129.,-15.,15.7));
#9870=CARTESIAN_POINT('',(129.3,-15.,16.));
#9871=CARTESIAN_POINT('Origin',(144.7,21.1999999999999,1.01948044689421));
#9872=CARTESIAN_POINT('',(145.,21.1999999999999,2.29525996204705));
#9873=CARTESIAN_POINT('',(145.,21.1999999999999,1.01948044689421));
#9874=CARTESIAN_POINT('',(144.7,21.4999999999999,2.03896089378841));
#9875=CARTESIAN_POINT('Ctrl Pts',(144.7,21.4999999999999,2.03896089378841));
#9876=CARTESIAN_POINT('Ctrl Pts',(144.729707021216,21.4999999999999,2.03896089378841));
#9877=CARTESIAN_POINT('Ctrl Pts',(144.758777673282,21.4955937057347,2.04285168076792));
#9878=CARTESIAN_POINT('Ctrl Pts',(144.817440852233,21.4779567710066,2.05836227087722));
#9879=CARTESIAN_POINT('Ctrl Pts',(144.845615509175,21.4640057619501,2.07060652861162));
#9880=CARTESIAN_POINT('Ctrl Pts',(144.902101216584,21.4250399915451,2.10457296342855));
#9881=CARTESIAN_POINT('Ctrl Pts',(144.927927434013,21.3982203268002,2.12780612534895));
#9882=CARTESIAN_POINT('Ctrl Pts',(144.964853191741,21.3441129754836,2.17419410934394));
#9883=CARTESIAN_POINT('Ctrl Pts',(144.977648024164,21.3172521646773,2.19704892779082));
#9884=CARTESIAN_POINT('Ctrl Pts',(144.995183002517,21.2612564013421,2.24427435401479));
#9885=CARTESIAN_POINT('Ctrl Pts',(144.99975020409,21.2318642099517,2.26885093208373));
#9886=CARTESIAN_POINT('Ctrl Pts',(144.999996676586,21.2016304842259,2.29390907945453));
#9887=CARTESIAN_POINT('Ctrl Pts',(145.,21.2008152808565,2.29458456963201));
#9888=CARTESIAN_POINT('Ctrl Pts',(145.,21.1999999999999,2.29525996204705));
#9889=CARTESIAN_POINT('',(144.7,21.4999999999999,1.01948044689421));
#9890=CARTESIAN_POINT('Origin',(141.,-21.1999999999999,15.7));
#9891=CARTESIAN_POINT('',(141.,-21.4999999999999,15.7));
#9892=CARTESIAN_POINT('',(141.,-21.1999999999999,16.));
#9893=CARTESIAN_POINT('Origin',(129.3,-21.1999999999999,1.01948044689421));
#9894=CARTESIAN_POINT('',(129.,-21.1999999999999,2.29525996204705));
#9895=CARTESIAN_POINT('',(129.,-21.1999999999999,1.01948044689421));
#9896=CARTESIAN_POINT('',(129.3,-21.4999999999999,2.03896089378841));
#9897=CARTESIAN_POINT('Ctrl Pts',(129.3,-21.4999999999999,2.03896089378841));
#9898=CARTESIAN_POINT('Ctrl Pts',(129.270292978784,-21.4999999999999,2.03896089378841));
#9899=CARTESIAN_POINT('Ctrl Pts',(129.241222326718,-21.4955937057347,2.04285168076791));
#9900=CARTESIAN_POINT('Ctrl Pts',(129.182559147767,-21.4779567710066,2.05836227087723));
#9901=CARTESIAN_POINT('Ctrl Pts',(129.154384490824,-21.4640057619501,2.07060652861162));
#9902=CARTESIAN_POINT('Ctrl Pts',(129.097898783416,-21.4250399915451,2.10457296342855));
#9903=CARTESIAN_POINT('Ctrl Pts',(129.072072565987,-21.3982203268002,2.12780612534895));
#9904=CARTESIAN_POINT('Ctrl Pts',(129.035146808259,-21.3441129754836,2.17419410934393));
#9905=CARTESIAN_POINT('Ctrl Pts',(129.022351975836,-21.3172521646773,2.19704892779082));
#9906=CARTESIAN_POINT('Ctrl Pts',(129.004816997483,-21.2612564013421,2.24427435401479));
#9907=CARTESIAN_POINT('Ctrl Pts',(129.000249795909,-21.2318642099517,2.26885093208373));
#9908=CARTESIAN_POINT('Ctrl Pts',(129.000003323414,-21.2016304842259,2.29390907945453));
#9909=CARTESIAN_POINT('Ctrl Pts',(129.,-21.2008152808565,2.29458456963201));
#9910=CARTESIAN_POINT('Ctrl Pts',(129.,-21.1999999999999,2.29525996204705));
#9911=CARTESIAN_POINT('',(129.3,-21.4999999999999,1.01948044689421));
#9912=CARTESIAN_POINT('Origin',(129.3,21.9999999999999,-1.92966607280848));
#9913=CARTESIAN_POINT('Origin',(129.3,21.9999999999999,-1.92966607280848));
#9914=CARTESIAN_POINT('Origin',(129.,21.9999999999999,-1.92966607280848));
#9915=CARTESIAN_POINT('Origin',(144.7,-21.1999999999999,1.01948044689421));
#9916=CARTESIAN_POINT('',(144.7,-21.4999999999999,2.03896089378841));
#9917=CARTESIAN_POINT('',(144.7,-21.4999999999999,1.01948044689421));
#9918=CARTESIAN_POINT('',(145.,-21.1999999999999,2.29525996204705));
#9919=CARTESIAN_POINT('Ctrl Pts',(145.,-21.1999999999999,2.29525996204705));
#9920=CARTESIAN_POINT('Ctrl Pts',(145.,-21.2008152808404,2.29458456964534));
#9921=CARTESIAN_POINT('Ctrl Pts',(144.999996676585,-21.2016304842412,2.29390907943587));
#9922=CARTESIAN_POINT('Ctrl Pts',(144.999750204092,-21.2318642097648,2.26885093228761));
#9923=CARTESIAN_POINT('Ctrl Pts',(144.995183002528,-21.2612564013074,2.24427435404393));
#9924=CARTESIAN_POINT('Ctrl Pts',(144.977648024164,-21.3172521646786,2.19704892778962));
#9925=CARTESIAN_POINT('Ctrl Pts',(144.964853191741,-21.3441129754842,2.17419410934337));
#9926=CARTESIAN_POINT('Ctrl Pts',(144.927927434013,-21.3982203268002,2.12780612534895));
#9927=CARTESIAN_POINT('Ctrl Pts',(144.902101216584,-21.4250399915451,2.10457296342854));
#9928=CARTESIAN_POINT('Ctrl Pts',(144.845615509175,-21.4640057619501,2.07060652861161));
#9929=CARTESIAN_POINT('Ctrl Pts',(144.817440852233,-21.4779567710066,2.05836227087722));
#9930=CARTESIAN_POINT('Ctrl Pts',(144.758777673282,-21.4955937057347,2.04285168076792));
#9931=CARTESIAN_POINT('Ctrl Pts',(144.729707021216,-21.4999999999999,2.03896089378841));
#9932=CARTESIAN_POINT('Ctrl Pts',(144.7,-21.4999999999999,2.03896089378841));
#9933=CARTESIAN_POINT('',(145.,-21.1999999999999,1.01948044689421));
#9934=CARTESIAN_POINT('Origin',(144.7,21.9999999999999,-1.92966607280848));
#9935=CARTESIAN_POINT('Origin',(145.,21.9999999999999,-1.92966607280848));
#9936=CARTESIAN_POINT('Origin',(144.7,21.9999999999999,-1.92966607280848));
#9937=CARTESIAN_POINT('Origin',(129.3,-21.9999999999999,-1.92966607280848));
#9938=CARTESIAN_POINT('Origin',(129.,-21.9999999999999,-1.92966607280848));
#9939=CARTESIAN_POINT('Origin',(129.3,-21.9999999999999,-1.92966607280848));
#9940=CARTESIAN_POINT('Origin',(144.7,-21.9999999999999,-1.92966607280848));
#9941=CARTESIAN_POINT('Origin',(144.7,-21.9999999999999,-1.92966607280848));
#9942=CARTESIAN_POINT('Origin',(145.,-21.9999999999999,-1.92966607280848));
#9943=CARTESIAN_POINT('Origin',(144.7,15.,15.7));
#9944=CARTESIAN_POINT('',(145.,15.,15.7));
#9945=CARTESIAN_POINT('',(144.7,15.,16.));
#9946=CARTESIAN_POINT('Origin',(141.,-22.7999999999999,15.7));
#9947=CARTESIAN_POINT('',(141.,-22.4999999999999,15.7));
#9948=CARTESIAN_POINT('',(141.,-22.7999999999999,16.));
#9949=CARTESIAN_POINT('Origin',(129.3,-15.,15.7));
#9950=CARTESIAN_POINT('',(129.,-15.,15.7));
#9951=CARTESIAN_POINT('',(129.3,-15.,16.));
#9952=CARTESIAN_POINT('Origin',(141.,-29.7,15.7));
#9953=CARTESIAN_POINT('',(141.,-30.,15.7));
#9954=CARTESIAN_POINT('',(141.,-29.7,16.));
#9955=CARTESIAN_POINT('Origin',(129.3,2.5,-10.3));
#9956=CARTESIAN_POINT('',(129.,2.5,-10.3));
#9957=CARTESIAN_POINT('Origin',(133.,30.3,-9.7));
#9958=CARTESIAN_POINT('',(133.,30.,-9.7));
#9959=CARTESIAN_POINT('Origin',(144.7,32.5,-10.3));
#9960=CARTESIAN_POINT('',(145.,32.5,-10.3));
#9961=CARTESIAN_POINT('Origin',(141.,-30.3,-9.7));
#9962=CARTESIAN_POINT('',(141.,-30.,-9.7));
#9963=CARTESIAN_POINT('Origin',(129.3,-32.5,-10.3));
#9964=CARTESIAN_POINT('',(129.,-32.5,-10.3));
#9965=CARTESIAN_POINT('Origin',(129.3,39.7,-8.));
#9966=CARTESIAN_POINT('',(129.3,40.,-8.));
#9967=CARTESIAN_POINT('',(129.,39.7,-8.));
#9968=CARTESIAN_POINT('Origin',(144.7,-2.5,-10.3));
#9969=CARTESIAN_POINT('',(145.,-2.5,-10.3));
#9970=CARTESIAN_POINT('Origin',(144.7,39.7,-8.));
#9971=CARTESIAN_POINT('',(145.,39.7,-8.));
#9972=CARTESIAN_POINT('',(144.7,40.,-8.));
#9973=CARTESIAN_POINT('Origin',(141.,-39.7,-10.3));
#9974=CARTESIAN_POINT('',(141.,-40.,-10.3));
#9975=CARTESIAN_POINT('Origin',(141.,-39.7,-15.7));
#9976=CARTESIAN_POINT('',(141.,-40.,-15.7));
#9977=CARTESIAN_POINT('',(141.,-39.7,-16.));
#9978=CARTESIAN_POINT('Origin',(145.,21.4999999999999,2.03896089378841));
#9979=CARTESIAN_POINT('',(145.,21.4999999999999,2.03896089378841));
#9980=CARTESIAN_POINT('Origin',(145.,21.9999999999999,-1.92966607280848));
#9981=CARTESIAN_POINT('',(145.,22.4999999999999,2.03896089378841));
#9982=CARTESIAN_POINT('Origin',(145.,-21.9999999999999,-1.92966607280848));
#9983=CARTESIAN_POINT('',(145.,-22.4999999999999,2.03896089378841));
#9984=CARTESIAN_POINT('',(145.,-21.4999999999999,2.03896089378841));
#9985=CARTESIAN_POINT('Origin',(145.,-21.4999999999999,2.03896089378841));
#9986=CARTESIAN_POINT('Origin',(137.,-4.44089209850063E-15,-16.));
#9987=CARTESIAN_POINT('Origin',(145.,-40.,-16.));
#9988=CARTESIAN_POINT('Origin',(145.,40.,-16.));
#9989=CARTESIAN_POINT('Origin',(145.,-30.,0.));
#9990=CARTESIAN_POINT('Origin',(137.,-4.44089209850063E-15,16.));
#9991=CARTESIAN_POINT('Origin',(129.,30.,0.));
#9992=CARTESIAN_POINT('Origin',(137.,-4.44089209850063E-15,16.));
#9993=CARTESIAN_POINT('Origin',(145.,30.,0.));
#9994=CARTESIAN_POINT('Origin',(137.,-4.44089209850063E-15,16.));
#9995=CARTESIAN_POINT('Origin',(129.,-30.,0.));
#9996=CARTESIAN_POINT('Origin',(145.,22.4999999999999,16.));
#9997=CARTESIAN_POINT('Origin',(145.,-22.4999999999999,16.));
#10620=UNCERTAINTY_MEASURE_WITH_UNIT(LENGTH_MEASURE(0.01),#10640,
'DISTANCE_ACCURACY_VALUE',
'Maximum model space distance between geometric entities at asserted c
onnectivities');
#10627=UNCERTAINTY_MEASURE_WITH_UNIT(LENGTH_MEASURE(0.01),#10640,
'DISTANCE_ACCURACY_VALUE',
'Maximum model space distance between geometric entities at asserted c
onnectivities');
#10632=(
GEOMETRIC_REPRESENTATION_CONTEXT(3)
GLOBAL_UNCERTAINTY_ASSIGNED_CONTEXT((#10620))
GLOBAL_UNIT_ASSIGNED_CONTEXT((#10640,#10642,#10643))
REPRESENTATION_CONTEXT('','3D')
);
#10639=(
GEOMETRIC_REPRESENTATION_CONTEXT(3)
GLOBAL_UNCERTAINTY_ASSIGNED_CONTEXT((#10627))
GLOBAL_UNIT_ASSIGNED_CONTEXT((#10640,#10642,#10643))
REPRESENTATION_CONTEXT('','3D')
);
#10640=(
LENGTH_UNIT()
NAMED_UNIT(*)
SI_UNIT(.MILLI.,.METRE.)
);
#10642=(
NAMED_UNIT(*)
PLANE_ANGLE_UNIT()
SI_UNIT($,.RADIAN.)
);
#10643=(
NAMED_UNIT(*)
SI_UNIT($,.STERADIAN.)
SOLID_ANGLE_UNIT()
);
#10648=SHAPE_DEFINITION_REPRESENTATION(#10659,#10680);
#10659=PRODUCT_DEFINITION_SHAPE('',$,#10692);
#10680=SHAPE_REPRESENTATION('',(#6224),#10632);
#10687=PRODUCT_DEFINITION_CONTEXT('part definition',#10722,'design');
#10692=PRODUCT_DEFINITION('End_Block','End_Block',#10703,#10687);
#10703=PRODUCT_DEFINITION_FORMATION('',$,#10728);
#10722=APPLICATION_CONTEXT(
'Core Data for Automotive Mechanical Design Process');
#10723=PRODUCT_CONTEXT('part definition',#10722,'mechanical');
#10728=PRODUCT('End_Block','End_Block',$,(#10723));
#10763=COLOUR_RGB('Dark Blue',0.08,0.2,0.34);
#10764=FILL_AREA_STYLE_COLOUR('',#10763);
#10765=FILL_AREA_STYLE('',(#10764));
#10766=SURFACE_STYLE_FILL_AREA(#10765);
#10767=SURFACE_SIDE_STYLE('',(#10766));
#10768=SURFACE_STYLE_USAGE(.BOTH.,#10767);
#10769=PRESENTATION_STYLE_ASSIGNMENT((#10768));
ENDSEC;
END-ISO-10303-21;
